ISO-10303-21;
HEADER;
FILE_DESCRIPTION (('STEP AP214'),
    '1' );
FILE_NAME ('pad arm left_left.step',
    '2026-10-08T07:58:12',
    ( '' ),
    ( '' ),
    'SwSTEP 2.0',
    'SolidWorks 2026',
    '' );
FILE_SCHEMA (( 'AUTOMOTIVE_DESIGN' ));
ENDSEC;

DATA;
#13=DIRECTION ( 'NONE',  ( 0.000000000000000000, 0.000000000000000000, 1.000000000000000000 ) ) ;
#25=DIRECTION ( 'NONE',  ( -1.000000000000000000, 0.000000000000000000, 0.000000000000000000 ) ) ;
#29=EDGE_CURVE ( 'NONE', #11107, #14777, #31364, .T. ) ;
#79=ORIENTED_EDGE ( 'NONE', *, *, #5370, .F. ) ;
#125=CARTESIAN_POINT ( 'NONE',  ( -56.25402757683428234, 194.9848779240976171, -1.110136720165091129 ) ) ;
#165=VECTOR ( 'NONE', #3398, 1000.000000000000000 ) ;
#172=DIRECTION ( 'NONE',  ( 0.000000000000000000, 0.000000000000000000, 1.000000000000000000 ) ) ;
#226=DIRECTION ( 'NONE',  ( 1.000000000000000000, 0.000000000000000000, 0.000000000000000000 ) ) ;
#227=EDGE_CURVE ( 'NONE', #17881, #23868, #23670, .T. ) ;
#245=STYLED_ITEM ( 'NONE', ( #10197 ), #10045 ) ;
#248=CARTESIAN_POINT ( 'NONE',  ( -64.50000000000000000, -95.00000000000000000, 270.4495957273638282 ) ) ;
#250=VERTEX_POINT ( 'NONE', #3251 ) ;
#319=ORIENTED_EDGE ( 'NONE', *, *, #6440, .F. ) ;
#325=FILL_AREA_STYLE ('',( #15500 ) ) ;
#335=EDGE_CURVE ( 'NONE', #14777, #31781, #18767, .T. ) ;
#345=DIRECTION ( 'NONE',  ( 0.000000000000000000, 0.000000000000000000, 1.000000000000000000 ) ) ;
#396=CARTESIAN_POINT ( 'NONE',  ( 60.63708498984762940, 120.3589838486224579, -20.00000000000000000 ) ) ;
#402=CARTESIAN_POINT ( 'NONE',  ( -52.50000000000002132, 155.0000000000000000, 6.938893903907228378E-15 ) ) ;
#428=ORIENTED_EDGE ( 'NONE', *, *, #4153, .F. ) ;
#472=CARTESIAN_POINT ( 'NONE',  ( -67.50000000000000000, 122.1366465496900418, -17.00000000000001421 ) ) ;
#508=CARTESIAN_POINT ( 'NONE',  ( -63.50000000000004263, 215.0000000000000000, 0.000000000000000000 ) ) ;
#518=CYLINDRICAL_SURFACE ( 'NONE', #15739, 17.00000000000000355 ) ;
#548=CARTESIAN_POINT ( 'NONE',  ( -58.50000000000001421, -88.00000000000000000, 20.00000000000000000 ) ) ;
#580=ORIENTED_EDGE ( 'NONE', *, *, #33085, .F. ) ;
#590=EDGE_CURVE ( 'NONE', #31987, #31739, #18056, .T. ) ;
#619=MANIFOLD_SOLID_BREP ( 'Boss-Extrude3', #29190 ) ;
#637=EDGE_CURVE ( 'NONE', #6050, #31294, #20445, .T. ) ;
#642=AXIS2_PLACEMENT_3D ( 'NONE', #23360, #10744, #31522 ) ;
#686=ORIENTED_EDGE ( 'NONE', *, *, #637, .T. ) ;
#688=DIRECTION ( 'NONE',  ( -0.000000000000000000, -0.000000000000000000, -1.000000000000000000 ) ) ;
#702=CARTESIAN_POINT ( 'NONE',  ( -60.87270596256635713, 194.9921970430798979, -0.8044259506661830539 ) ) ;
#858=EDGE_CURVE ( 'NONE', #11477, #33308, #3671, .T. ) ;
#868=CARTESIAN_POINT ( 'NONE',  ( -60.48814638060569848, 194.9711715815534205, -1.524404325634890700 ) ) ;
#922=VECTOR ( 'NONE', #2392, 1000.000000000000114 ) ;
#930=VECTOR ( 'NONE', #7597, 1000.000000000000114 ) ;
#945=EDGE_CURVE ( 'NONE', #28898, #31739, #6447, .T. ) ;
#968=VECTOR ( 'NONE', #31908, 1000.000000000000000 ) ;
#1019=FACE_OUTER_BOUND ( 'NONE', #22833, .T. ) ;
#1024=ORIENTED_EDGE ( 'NONE', *, *, #32635, .F. ) ;
#1026=VECTOR ( 'NONE', #8266, 1000.000000000000000 ) ;
#1041=CARTESIAN_POINT ( 'NONE',  ( -60.91993774119386984, 194.9950632347986641, -0.6485596632537811157 ) ) ;
#1049=CIRCLE ( 'NONE', #20059, 2.500000000000000000 ) ;
#1071=DIRECTION ( 'NONE',  ( -0.000000000000000000, -0.000000000000000000, -1.000000000000000000 ) ) ;
#1076=CIRCLE ( 'NONE', #10334, 2.500000000000000000 ) ;
#1100=LINE ( 'NONE', #11492, #1026 ) ;
#1116=ORIENTED_EDGE ( 'NONE', *, *, #8477, .T. ) ;
#1119=ORIENTED_EDGE ( 'NONE', *, *, #227, .T. ) ;
#1192=CARTESIAN_POINT ( 'NONE',  ( -64.50000000000000000, 2.605762844159070557, -20.00000000000000000 ) ) ;
#1291=VERTEX_POINT ( 'NONE', #14067 ) ;
#1368=ORIENTED_EDGE ( 'NONE', *, *, #590, .T. ) ;
#1456=CARTESIAN_POINT ( 'NONE',  ( -67.50000000000000000, 155.0000000000000000, 6.938893903907228378E-15 ) ) ;
#1602=CARTESIAN_POINT ( 'NONE',  ( -68.50000000000000000, 215.0000000000000000, 0.000000000000000000 ) ) ;
#1644=CARTESIAN_POINT ( 'NONE',  ( -64.50000000000000000, -2.605762844159085212, -20.00000000000000000 ) ) ;
#1662=DIRECTION ( 'NONE',  ( -1.000000000000000000, 0.000000000000000000, 0.000000000000000000 ) ) ;
#1668=LINE ( 'NONE', #12060, #4955 ) ;
#1700=ORIENTED_EDGE ( 'NONE', *, *, #14373, .T. ) ;
#1728=CARTESIAN_POINT ( 'NONE',  ( -64.50000000000000000, -2.605762844159085212, -20.00000000000000000 ) ) ;
#1735=( BOUNDED_CURVE ( )  B_SPLINE_CURVE ( 3, ( #25427, #23389, #4815, #2266 ),
 .UNSPECIFIED., .F., .T. ) 
 B_SPLINE_CURVE_WITH_KNOTS ( ( 4, 4 ),
 ( 5.758306373677911871, 6.283185307179586232 ),
 .UNSPECIFIED. ) 
 CURVE ( )  GEOMETRIC_REPRESENTATION_ITEM ( )  RATIONAL_B_SPLINE_CURVE ( ( 1.000000000000000000, 0.9771733092046011038, 0.9771733092046011038, 1.000000000000000000 ) ) 
 REPRESENTATION_ITEM ( '' )  );
#1766=CIRCLE ( 'NONE', #13181, 5.200000000000009948 ) ;
#1770=ORIENTED_EDGE ( 'NONE', *, *, #945, .T. ) ;
#1821=EDGE_LOOP ( 'NONE', ( #1119, #3453 ) ) ;
#1849=CARTESIAN_POINT ( 'NONE',  ( -54.50000000000002132, 155.0000000000000000, 17.00000000000001421 ) ) ;
#2084=DIRECTION ( 'NONE',  ( 1.000000000000000000, 0.000000000000000000, 0.000000000000000000 ) ) ;
#2085=VERTEX_POINT ( 'NONE', #24212 ) ;
#2110=AXIS2_PLACEMENT_3D ( 'NONE', #33217, #15659, #26059 ) ;
#2116=CARTESIAN_POINT ( 'NONE',  ( -96.16666666666678509, -63.33333333333321491, 11.66666666666661278 ) ) ;
#2142=CARTESIAN_POINT ( 'NONE',  ( -125.0000000000000000, 0.000000000000000000, 20.00000000000000000 ) ) ;
#2178=CARTESIAN_POINT ( 'NONE',  ( -56.12844631811822893, 194.9921284422999292, -0.8077925457893648797 ) ) ;
#2215=DIRECTION ( 'NONE',  ( 0.000000000000000000, 0.000000000000000000, 1.000000000000000000 ) ) ;
#2255=ORIENTED_EDGE ( 'NONE', *, *, #17675, .F. ) ;
#2266=CARTESIAN_POINT ( 'NONE',  ( -65.20000000000000284, -7.347880794884118356E-15, 19.29999999999998295 ) ) ;
#2341=ORIENTED_EDGE ( 'NONE', *, *, #32267, .F. ) ;
#2344=ORIENTED_EDGE ( 'NONE', *, *, #21993, .T. ) ;
#2347=CARTESIAN_POINT ( 'NONE',  ( -56.84624105109630676, 194.9558714263463912, 1.881936590917415941 ) ) ;
#2381=VERTEX_POINT ( 'NONE', #14997 ) ;
#2392=DIRECTION ( 'NONE',  ( 0.7071067811865474617, 8.659560562354932858E-17, 0.7071067811865474617 ) ) ;
#2404=AXIS2_PLACEMENT_3D ( 'NONE', #8872, #11941, #4266 ) ;
#2466=CARTESIAN_POINT ( 'NONE',  ( -52.50000000000002132, 155.0000000000000000, 6.938893903907228378E-15 ) ) ;
#2474=VERTEX_POINT ( 'NONE', #26072 ) ;
#2477=CARTESIAN_POINT ( 'NONE',  ( -67.50000000000000000, 155.0000000000000000, -37.00000000000000000 ) ) ;
#2491=PLANE ( 'NONE',  #18442 ) ;
#2518=ADVANCED_FACE ( 'NONE', ( #31513 ), #5609, .T. ) ;
#2682=ORIENTED_EDGE ( 'NONE', *, *, #14249, .T. ) ;
#2692=CARTESIAN_POINT ( 'NONE',  ( -56.08018104464575515, 194.9950560901275480, -0.6488614982153378952 ) ) ;
#2736=SURFACE_STYLE_USAGE ( .BOTH. , #23170 ) ;
#2740=CARTESIAN_POINT ( 'NONE',  ( -67.50000000000000000, 155.0000000000000000, 6.938893903907228378E-15 ) ) ;
#2753=CARTESIAN_POINT ( 'NONE',  ( 60.63708498984762940, 155.0000000000000000, 6.938893903907228378E-15 ) ) ;
#2757=DIRECTION ( 'NONE',  ( 1.000000000000000000, 0.000000000000000000, 0.000000000000000000 ) ) ;
#2764=ADVANCED_FACE ( 'NONE', ( #24506 ), #32337, .F. ) ;
#2776=ORIENTED_EDGE ( 'NONE', *, *, #33029, .F. ) ;
#2803=ORIENTED_EDGE ( 'NONE', *, *, #31409, .F. ) ;
#2845=CARTESIAN_POINT ( 'NONE',  ( -56.07926260655170836, 194.9951118559247050, 0.6454098859825110335 ) ) ;
#2894=CIRCLE ( 'NONE', #17014, 40.00000000000000711 ) ;
#2926=AXIS2_PLACEMENT_3D ( 'NONE', #28536, #33639, #10810 ) ;
#2987=CARTESIAN_POINT ( 'NONE',  ( -63.49999999999884892, 215.0000000000000000, 2.500000000000000000 ) ) ;
#2991=PLANE ( 'NONE',  #32035 ) ;
#3014=DIRECTION ( 'NONE',  ( -0.000000000000000000, -0.000000000000000000, -1.000000000000000000 ) ) ;
#3069=CONICAL_SURFACE ( 'NONE', #17218, 37.00000000000000711, 0.7853981633974482790 ) ;
#3072=CARTESIAN_POINT ( 'NONE',  ( -64.50000000000000000, -95.00000000000000000, -20.00000000000000000 ) ) ;
#3094=DIRECTION ( 'NONE',  ( 0.000000000000000000, 0.000000000000000000, 1.000000000000000000 ) ) ;
#3127=EDGE_CURVE ( 'NONE', #31781, #25951, #1668, .T. ) ;
#3228=LINE ( 'NONE', #10911, #14173 ) ;
#3239=EDGE_LOOP ( 'NONE', ( #11599, #32199, #15689, #23418, #19046, #29609 ) ) ;
#3247=CARTESIAN_POINT ( 'NONE',  ( -67.50000000000000000, 155.0000000000000000, 6.938893903907228378E-15 ) ) ;
#3251=CARTESIAN_POINT ( 'NONE',  ( -64.50000000000000000, 155.0000000000000000, -40.00000000000000000 ) ) ;
#3363=DIRECTION ( 'NONE',  ( 0.000000000000000000, 0.000000000000000000, 1.000000000000000000 ) ) ;
#3388=CIRCLE ( 'NONE', #6656, 4.199999999999988631 ) ;
#3398=DIRECTION ( 'NONE',  ( -1.000000000000000000, 0.000000000000000000, 0.000000000000000000 ) ) ;
#3416=CARTESIAN_POINT ( 'NONE',  ( -60.02418147676856108, 194.9506531851598936, 1.988357156115594826 ) ) ;
#3444=LINE ( 'NONE', #396, #14264 ) ;
#3453=ORIENTED_EDGE ( 'NONE', *, *, #20858, .T. ) ;
#3502=VERTEX_POINT ( 'NONE', #28590 ) ;
#3584=ORIENTED_EDGE ( 'NONE', *, *, #29596, .T. ) ;
#3586=CARTESIAN_POINT ( 'NONE',  ( -60.15281075484971041, 194.9558321103198466, 1.882765505879504309 ) ) ;
#3597=DIRECTION ( 'NONE',  ( 0.000000000000000000, -1.000000000000000000, 0.000000000000000000 ) ) ;
#3671=CIRCLE ( 'NONE', #25983, 17.00000000000000355 ) ;
#3690=PRODUCT ( 'pad arm left_left', 'pad arm left_left', '', ( #9901 ) ) ;
#3762=CARTESIAN_POINT ( 'NONE',  ( -67.50000000000000000, 0.000000000000000000, -17.00000000000001421 ) ) ;
#3800=ORIENTED_EDGE ( 'NONE', *, *, #20647, .T. ) ;
#3802=DIRECTION ( 'NONE',  ( 0.000000000000000000, 0.000000000000000000, -1.000000000000000000 ) ) ;
#3956=VECTOR ( 'NONE', #13183, 1000.000000000000000 ) ;
#3965=FACE_BOUND ( 'NONE', #23733, .T. ) ;
#3996=CIRCLE ( 'NONE', #31200, 4.199999999999988631 ) ;
#4015=DIRECTION ( 'NONE',  ( -0.000000000000000000, -0.000000000000000000, -1.000000000000000000 ) ) ;
#4045=VERTEX_POINT ( 'NONE', #20501 ) ;
#4091=ORIENTED_EDGE ( 'NONE', *, *, #17878, .F. ) ;
#4153=EDGE_CURVE ( 'NONE', #17881, #13027, #21000, .T. ) ;
#4183=AXIS2_PLACEMENT_3D ( 'NONE', #1456, #15576, #22577 ) ;
#4198=AXIS2_PLACEMENT_3D ( 'NONE', #17897, #25895, #20622 ) ;
#4266=DIRECTION ( 'NONE',  ( 1.000000000000000000, 0.000000000000000000, 0.000000000000000000 ) ) ;
#4286=CARTESIAN_POINT ( 'NONE',  ( -52.50000000000002132, 155.0000000000000000, 6.938893903907228378E-15 ) ) ;
#4423=ORIENTED_EDGE ( 'NONE', *, *, #26819, .T. ) ;
#4456=B_SPLINE_CURVE_WITH_KNOTS ( 'NONE', 3,
 ( #25551, #12598, #23663, #20616 ),
 .UNSPECIFIED., .F., .F.,
 ( 4, 4 ),
 ( 0.000000000000000000, 0.004600009204204579850 ),
 .UNSPECIFIED. ) ;
#4494=CYLINDRICAL_SURFACE ( 'NONE', #20634, 2.500000000000000000 ) ;
#4510=VERTEX_POINT ( 'NONE', #11121 ) ;
#4663=DIRECTION ( 'NONE',  ( 0.000000000000000000, 1.000000000000000000, 0.000000000000000000 ) ) ;
#4704=CIRCLE ( 'NONE', #17769, 2.500000000000000000 ) ;
#4720=AXIS2_PLACEMENT_3D ( 'NONE', #8649, #11206, #3363 ) ;
#4728=ORIENTED_EDGE ( 'NONE', *, *, #20197, .T. ) ;
#4729=AXIS2_PLACEMENT_3D ( 'NONE', #2142, #12690, #15073 ) ;
#4759=VECTOR ( 'NONE', #4663, 1000.000000000000000 ) ;
#4784=CARTESIAN_POINT ( 'NONE',  ( -67.50000000000000000, 122.1366465496900418, -17.00000000000001421 ) ) ;
#4815=CARTESIAN_POINT ( 'NONE',  ( -65.20000000000000284, 0.9203920079924619024, 19.30000000000001847 ) ) ;
#4875=LINE ( 'NONE', #33666, #14061 ) ;
#4895=EDGE_LOOP ( 'NONE', ( #10562, #15791, #29430, #25406 ) ) ;
#4898=CARTESIAN_POINT ( 'NONE',  ( -56.61815514298172758, 194.9659613751070140, -1.653849335561433209 ) ) ;
#4955=VECTOR ( 'NONE', #22448, 1000.000000000000000 ) ;
#4973=CARTESIAN_POINT ( 'NONE',  ( -67.50000000000000000, 155.0000000000000000, 6.938893903907228378E-15 ) ) ;
#4985=EDGE_CURVE ( 'NONE', #2381, #2474, #26153, .T. ) ;
#5026=DIRECTION ( 'NONE',  ( 0.000000000000000000, 0.000000000000000000, 1.000000000000000000 ) ) ;
#5028=LINE ( 'NONE', #2477, #930 ) ;
#5089=CARTESIAN_POINT ( 'NONE',  ( -58.50000000000002132, 209.9999999999999716, -2.500000000000000000 ) ) ;
#5218=EDGE_CURVE ( 'NONE', #19176, #25951, #3228, .T. ) ;
#5304=ORIENTED_EDGE ( 'NONE', *, *, #11411, .T. ) ;
#5351=ADVANCED_FACE ( 'NONE', ( #31682 ), #518, .F. ) ;
#5370=EDGE_CURVE ( 'NONE', #6050, #28898, #26683, .T. ) ;
#5465=CARTESIAN_POINT ( 'NONE',  ( -67.50000000000000000, 155.0000000000000000, 37.00000000000001421 ) ) ;
#5466=CARTESIAN_POINT ( 'NONE',  ( -63.49999999999884892, 215.0000000000003979, 0.000000000000000000 ) ) ;
#5495=DIRECTION ( 'NONE',  ( 0.000000000000000000, 1.000000000000000000, 0.000000000000000000 ) ) ;
#5592=CYLINDRICAL_SURFACE ( 'NONE', #4720, 2.500000000000000000 ) ;
#5607=VECTOR ( 'NONE', #14871, 1000.000000000000000 ) ;
#5609=CYLINDRICAL_SURFACE ( 'NONE', #20641, 2.500000000000000000 ) ;
#5625=EDGE_CURVE ( 'NONE', #1291, #31987, #31455, .T. ) ;
#5669=ORIENTED_EDGE ( 'NONE', *, *, #29910, .T. ) ;
#5679=VERTEX_POINT ( 'NONE', #23250 ) ;
#5800=CARTESIAN_POINT ( 'NONE',  ( -58.66318290517560996, 194.9217985566783113, -2.499999999999999556 ) ) ;
#5830=VECTOR ( 'NONE', #7513, 1000.000000000000000 ) ;
#5854=EDGE_CURVE ( 'NONE', #5679, #27924, #29031, .T. ) ;
#5934=CARTESIAN_POINT ( 'NONE',  ( -58.50000000000001421, -88.00000000000000000, -20.00000000000000000 ) ) ;
#5947=AXIS2_PLACEMENT_3D ( 'NONE', #4286, #14675, #25069 ) ;
#5957=ORIENTED_EDGE ( 'NONE', *, *, #27883, .F. ) ;
#5971=CARTESIAN_POINT ( 'NONE',  ( -59.60814253741918378, 194.9368883388851259, -2.246975524854183170 ) ) ;
#6015=CARTESIAN_POINT ( 'NONE',  ( -62.70000000000000284, -88.00000000000000000, -20.00000000000000000 ) ) ;
#6050=VERTEX_POINT ( 'NONE', #22358 ) ;
#6052=ORIENTED_EDGE ( 'NONE', *, *, #8738, .F. ) ;
#6107=DIRECTION ( 'NONE',  ( 0.000000000000000000, 1.000000000000000000, 0.000000000000000000 ) ) ;
#6136=VECTOR ( 'NONE', #28364, 1000.000000000000000 ) ;
#6137=CARTESIAN_POINT ( 'NONE',  ( -58.50000000000002132, 194.9217985566782829, -2.500000000000000000 ) ) ;
#6168=CARTESIAN_POINT ( 'NONE',  ( -58.50000000000001421, -88.00000000000000000, 20.00000000000000000 ) ) ;
#6235=PRODUCT_DEFINITION ( 'UNKNOWN', '', #7214, #9070 ) ;
#6305=CARTESIAN_POINT ( 'NONE',  ( -60.99994150909498103, 194.9999963443187028, 0.1639972282098350886 ) ) ;
#6308=ORIENTED_EDGE ( 'NONE', *, *, #18720, .T. ) ;
#6440=EDGE_CURVE ( 'NONE', #31548, #32869, #16241, .T. ) ;
#6447=LINE ( 'NONE', #30117, #15645 ) ;
#6485=CIRCLE ( 'NONE', #29883, 2.500000000000000000 ) ;
#6490=CARTESIAN_POINT ( 'NONE',  ( -60.15146012614710003, 194.9557722165940845, -1.884122726181822971 ) ) ;
#6601=ORIENTED_EDGE ( 'NONE', *, *, #5218, .T. ) ;
#6607=DIRECTION ( 'NONE',  ( -1.000000000000000000, 0.000000000000000000, 0.000000000000000000 ) ) ;
#6656=AXIS2_PLACEMENT_3D ( 'NONE', #548, #3094, #21651 ) ;
#6782=DIRECTION ( 'NONE',  ( 0.000000000000000000, -1.000000000000000000, 0.000000000000000000 ) ) ;
#6810=EDGE_LOOP ( 'NONE', ( #2776, #9117, #319, #4728, #16479, #25371 ) ) ;
#6814=CARTESIAN_POINT ( 'NONE',  ( -54.50000000000002132, 155.0000000000000000, -17.00000000000000000 ) ) ;
#6882=CYLINDRICAL_SURFACE ( 'NONE', #9197, 40.00000000000000711 ) ;
#6903=ADVANCED_FACE ( 'NONE', ( #25827 ), #2491, .T. ) ;
#6940=ORIENTED_EDGE ( 'NONE', *, *, #10432, .T. ) ;
#6951=ORIENTED_EDGE ( 'NONE', *, *, #16005, .F. ) ;
#7069=LINE ( 'NONE', #248, #3956 ) ;
#7093=DIRECTION ( 'NONE',  ( -1.000000000000000000, -0.000000000000000000, 0.000000000000000000 ) ) ;
#7112=VERTEX_POINT ( 'NONE', #2987 ) ;
#7123=DIRECTION ( 'NONE',  ( 0.000000000000000000, 0.000000000000000000, -1.000000000000000000 ) ) ;
#7124=FILL_AREA_STYLE_COLOUR ( '', #14916 ) ;
#7214=PRODUCT_DEFINITION_FORMATION_WITH_SPECIFIED_SOURCE ( 'ANY', '', #3690, .NOT_KNOWN. ) ;
#7250=AXIS2_PLACEMENT_3D ( 'NONE', #31556, #226, #23882 ) ;
#7287=ORIENTED_EDGE ( 'NONE', *, *, #13269, .F. ) ;
#7294=CARTESIAN_POINT ( 'NONE',  ( -67.50000000000000000, -92.00000000000000000, 17.00000000000001421 ) ) ;
#7308=EDGE_CURVE ( 'NONE', #4045, #3502, #1100, .T. ) ;
#7332=CIRCLE ( 'NONE', #33441, 40.00000000000000711 ) ;
#7335=ADVANCED_FACE ( 'NONE', ( #14386 ), #4494, .T. ) ;
#7363=DIRECTION ( 'NONE',  ( -1.000000000000000000, 0.000000000000000000, 0.000000000000000000 ) ) ;
#7459=CARTESIAN_POINT ( 'NONE',  ( -56.12712552280034117, 194.9922069576863066, 0.8039670099889266730 ) ) ;
#7466=SURFACE_STYLE_FILL_AREA ( #30464 ) ;
#7467=DIRECTION ( 'NONE',  ( 0.000000000000000000, 0.000000000000000000, -1.000000000000000000 ) ) ;
#7501=EDGE_CURVE ( 'NONE', #29388, #30979, #1049, .T. ) ;
#7513=DIRECTION ( 'NONE',  ( -1.000000000000000000, 0.000000000000000000, 0.000000000000000000 ) ) ;
#7530=ADVANCED_FACE ( 'NONE', ( #22378 ), #6882, .T. ) ;
#7559=AXIS2_PLACEMENT_3D ( 'NONE', #20749, #7812, #15634 ) ;
#7597=DIRECTION ( 'NONE',  ( 0.7071067811865474617, 0.000000000000000000, -0.7071067811865474617 ) ) ;
#7634=CARTESIAN_POINT ( 'NONE',  ( -57.69437687863553776, 194.9296432668266732, -2.372230612754127499 ) ) ;
#7769=AXIS2_PLACEMENT_3D ( 'NONE', #13707, #32277, #11504 ) ;
#7812=DIRECTION ( 'NONE',  ( 0.000000000000000000, -1.000000000000000000, 0.000000000000000000 ) ) ;
#7913=EDGE_LOOP ( 'NONE', ( #6052, #24624, #29853, #24629, #19097, #24379, #25639 ) ) ;
#8001=COLOUR_RGB ( '', 0.09019608, 0.27058824, 0.51372549) ;
#8107=ADVANCED_FACE ( 'NONE', ( #16891 ), #14175, .F. ) ;
#8126=CIRCLE ( 'NONE', #24428, 2.500000000000000000 ) ;
#8211=CYLINDRICAL_SURFACE ( 'NONE', #13776, 2.500000000000000000 ) ;
#8266=DIRECTION ( 'NONE',  ( -0.000000000000000000, -0.000000000000000000, -1.000000000000000000 ) ) ;
#8326=ORIENTED_EDGE ( 'NONE', *, *, #15823, .F. ) ;
#8327=VERTEX_POINT ( 'NONE', #33417 ) ;
#8419=CARTESIAN_POINT ( 'NONE',  ( -64.50000000000000000, 155.0000000000000000, 6.938893903907228378E-15 ) ) ;
#8477=EDGE_CURVE ( 'NONE', #7112, #10267, #1076, .T. ) ;
#8513=LINE ( 'NONE', #21791, #13735 ) ;
#8527=FACE_OUTER_BOUND ( 'NONE', #22213, .T. ) ;
#8539=MECHANICAL_DESIGN_GEOMETRIC_PRESENTATION_REPRESENTATION('',(#11796),#22696);
#8568=VERTEX_POINT ( 'NONE', #26089 ) ;
#8611=VERTEX_POINT ( 'NONE', #3072 ) ;
#8649=CARTESIAN_POINT ( 'NONE',  ( -58.50000000000002132, 185.0000000000000000, 0.000000000000000000 ) ) ;
#8688=EDGE_LOOP ( 'NONE', ( #5957, #23120, #29181, #3800, #12859 ) ) ;
#8704=CARTESIAN_POINT ( 'NONE',  ( -60.02503143742045921, 194.9506873066471542, -1.987662087495396301 ) ) ;
#8709=CARTESIAN_POINT ( 'NONE',  ( -125.0000000000000000, -95.00000000000000000, -20.00000000000000000 ) ) ;
#8738=EDGE_CURVE ( 'NONE', #16522, #6050, #22468, .T. ) ;
#8772=FACE_OUTER_BOUND ( 'NONE', #23582, .T. ) ;
#8799=CARTESIAN_POINT ( 'NONE',  ( -68.50000000000000000, 215.0000000000000000, 2.500000000000000000 ) ) ;
#8836=DIRECTION ( 'NONE',  ( -1.000000000000000000, -0.000000000000000000, -0.000000000000000000 ) ) ;
#8872=CARTESIAN_POINT ( 'NONE',  ( 0.000000000000000000, 0.000000000000000000, 0.000000000000000000 ) ) ;
#9017=CARTESIAN_POINT ( 'NONE',  ( -64.50000000000000000, 2.605762844159070557, -20.00000000000000000 ) ) ;
#9034=CARTESIAN_POINT ( 'NONE',  ( -58.82767890163440683, 194.9228235633793815, 2.483781759962022218 ) ) ;
#9058=CARTESIAN_POINT ( 'NONE',  ( -64.50000000000000000, 0.000000000000000000, -20.00000000000000000 ) ) ;
#9070=PRODUCT_DEFINITION_CONTEXT ( 'detailed design', #31616, 'design' ) ;
#9117=ORIENTED_EDGE ( 'NONE', *, *, #30631, .F. ) ;
#9136=( BOUNDED_CURVE ( )  B_SPLINE_CURVE ( 3, ( #12246, #32352, #19745, #9017 ),
 .UNSPECIFIED., .F., .T. ) 
 B_SPLINE_CURVE_WITH_KNOTS ( ( 4, 4 ),
 ( 3.141592653589793116, 3.666471587091465700 ),
 .UNSPECIFIED. ) 
 CURVE ( )  GEOMETRIC_REPRESENTATION_ITEM ( )  RATIONAL_B_SPLINE_CURVE ( ( 1.000000000000000000, 0.9771733092046011038, 0.9771733092046011038, 1.000000000000000000 ) ) 
 REPRESENTATION_ITEM ( '' )  );
#9138=DIRECTION ( 'NONE',  ( -1.000000000000000000, -0.000000000000000000, 0.000000000000000000 ) ) ;
#9197=AXIS2_PLACEMENT_3D ( 'NONE', #17272, #9604, #27661 ) ;
#9287=ORIENTED_EDGE ( 'NONE', *, *, #11474, .F. ) ;
#9326=DIRECTION ( 'NONE',  ( 0.000000000000000000, -1.000000000000000000, 0.000000000000000000 ) ) ;
#9406=TOROIDAL_SURFACE ( 'NONE', #32791, 4.999999999999990230, 2.500000000000000000 ) ;
#9480=DIRECTION ( 'NONE',  ( 0.000000000000000000, 0.000000000000000000, -1.000000000000000000 ) ) ;
#9603=EDGE_LOOP ( 'NONE', ( #16588, #18916, #30495, #25047 ) ) ;
#9604=DIRECTION ( 'NONE',  ( -1.000000000000000000, 0.000000000000000000, 0.000000000000000000 ) ) ;
#9638=CARTESIAN_POINT ( 'NONE',  ( -54.50000000000002132, 155.0000000000000000, 6.938893903907228378E-15 ) ) ;
#9666=CARTESIAN_POINT ( 'NONE',  ( -58.50000000000002132, 194.9217985566782829, -2.500000000000000000 ) ) ;
#9673=CARTESIAN_POINT ( 'NONE',  ( -63.49999999999884892, 215.0000000000003979, 0.000000000000000000 ) ) ;
#9676=AXIS2_PLACEMENT_3D ( 'NONE', #18577, #32012, #28961 ) ;
#9771=LINE ( 'NONE', #16619, #5607 ) ;
#9880=EDGE_CURVE ( 'NONE', #31294, #19176, #23174, .T. ) ;
#9901=PRODUCT_CONTEXT ( 'NONE', #28786, 'mechanical' ) ;
#9910=LINE ( 'NONE', #23366, #24640 ) ;
#9914=ORIENTED_EDGE ( 'NONE', *, *, #9988, .F. ) ;
#9925=DIRECTION ( 'NONE',  ( 1.000000000000000000, 0.000000000000000000, 0.000000000000000000 ) ) ;
#9957=ADVANCED_FACE ( 'NONE', ( #20950 ), #15167, .F. ) ;
#9988=EDGE_CURVE ( 'NONE', #31987, #11107, #24333, .T. ) ;
#10045=ADVANCED_BREP_SHAPE_REPRESENTATION ( '', ( #619, #2404 ), #29608 ) ;
#10080=DIRECTION ( 'NONE',  ( 0.000000000000000000, -1.000000000000000000, 0.000000000000000000 ) ) ;
#10122=CARTESIAN_POINT ( 'NONE',  ( -58.50000000000002132, 185.0000000000000000, -2.500000000000000000 ) ) ;
#10135=DIRECTION ( 'NONE',  ( -1.000000000000000000, 0.000000000000000000, 0.000000000000000000 ) ) ;
#10143=VERTEX_POINT ( 'NONE', #14108 ) ;
#10195=VECTOR ( 'NONE', #20365, 1000.000000000000000 ) ;
#10197=PRESENTATION_STYLE_ASSIGNMENT (( #30804 ) ) ;
#10216=VECTOR ( 'NONE', #22722, 1000.000000000000114 ) ;
#10226=VECTOR ( 'NONE', #18617, 1000.000000000000000 ) ;
#10239=( LENGTH_UNIT ( ) NAMED_UNIT ( * ) SI_UNIT ( .MILLI., .METRE. ) );
#10240=CONICAL_SURFACE ( 'NONE', #22180, 37.00000000000000711, 0.7853981633974482790 ) ;
#10256=CARTESIAN_POINT ( 'NONE',  ( -65.50384660342780307, 120.9385549553365848, -18.99615339657220758 ) ) ;
#10267=VERTEX_POINT ( 'NONE', #27893 ) ;
#10309=DIRECTION ( 'NONE',  ( 0.000000000000000000, 0.000000000000000000, 1.000000000000000000 ) ) ;
#10313=CARTESIAN_POINT ( 'NONE',  ( -64.50000000000000000, -2.605762844159085212, 20.00000000000000000 ) ) ;
#10325=ORIENTED_EDGE ( 'NONE', *, *, #12185, .T. ) ;
#10334=AXIS2_PLACEMENT_3D ( 'NONE', #5466, #2757, #24020 ) ;
#10355=ORIENTED_EDGE ( 'NONE', *, *, #4985, .F. ) ;
#10362=CARTESIAN_POINT ( 'NONE',  ( -56.96409840163092753, 194.9506684299840913, -1.999309141333601492 ) ) ;
#10368=EDGE_CURVE ( 'NONE', #2085, #25209, #12057, .T. ) ;
#10432=EDGE_CURVE ( 'NONE', #25081, #10143, #30325, .T. ) ;
#10484=ORIENTED_EDGE ( 'NONE', *, *, #15948, .F. ) ;
#10528=CARTESIAN_POINT ( 'NONE',  ( -57.39039945611308013, 194.9369330859559284, 2.246172506675526481 ) ) ;
#10552=CIRCLE ( 'NONE', #23598, 4.199999999999988631 ) ;
#10562=ORIENTED_EDGE ( 'NONE', *, *, #32280, .F. ) ;
#10594=DIRECTION ( 'NONE',  ( 0.000000000000000000, 0.000000000000000000, -1.000000000000000000 ) ) ;
#10639=DIRECTION ( 'NONE',  ( 0.000000000000000000, 0.000000000000000000, 1.000000000000000000 ) ) ;
#10715=FACE_OUTER_BOUND ( 'NONE', #8688, .T. ) ;
#10744=DIRECTION ( 'NONE',  ( 1.000000000000000000, 0.000000000000000000, 0.000000000000000000 ) ) ;
#10771=EDGE_CURVE ( 'NONE', #31294, #25209, #23633, .T. ) ;
#10799=DIRECTION ( 'NONE',  ( 0.000000000000000000, 0.000000000000000000, 1.000000000000000000 ) ) ;
#10810=DIRECTION ( 'NONE',  ( -0.000000000000000000, 0.000000000000000000, -1.000000000000000000 ) ) ;
#10863=CARTESIAN_POINT ( 'NONE',  ( -67.50000000000000000, -92.00000000000000000, -17.00000000000001421 ) ) ;
#10883=VECTOR ( 'NONE', #32353, 1000.000000000000000 ) ;
#10910=PLANE ( 'NONE',  #13827 ) ;
#10911=CARTESIAN_POINT ( 'NONE',  ( -98.16666666666678509, -61.33333333333321491, -13.66666666666659502 ) ) ;
#10932=DIRECTION ( 'NONE',  ( 0.000000000000000000, 0.000000000000000000, 1.000000000000000000 ) ) ;
#10975=EDGE_LOOP ( 'NONE', ( #79, #686, #32246, #12680, #4091, #19254 ) ) ;
#11020=EDGE_CURVE ( 'NONE', #16522, #15028, #9771, .T. ) ;
#11104=CARTESIAN_POINT ( 'NONE',  ( -59.60884549136632415, 194.9369081818307166, 2.246623501397673639 ) ) ;
#11107=VERTEX_POINT ( 'NONE', #30899 ) ;
#11121=CARTESIAN_POINT ( 'NONE',  ( -64.50000000000000000, 120.3589838486224579, -20.00000000000000000 ) ) ;
#11175=ORIENTED_EDGE ( 'NONE', *, *, #10432, .F. ) ;
#11206=DIRECTION ( 'NONE',  ( 0.000000000000000000, 1.000000000000000000, 0.000000000000000000 ) ) ;
#11211=ADVANCED_FACE ( 'NONE', ( #28998 ), #28509, .F. ) ;
#11230=DIRECTION ( 'NONE',  ( 0.000000000000000000, -1.000000000000000000, 0.000000000000000000 ) ) ;
#11233=CARTESIAN_POINT ( 'NONE',  ( -52.50000000000002132, 155.0000000000000000, -40.00000000000000000 ) ) ;
#11240=DIRECTION ( 'NONE',  ( -0.000000000000000000, -0.000000000000000000, -1.000000000000000000 ) ) ;
#11263=CARTESIAN_POINT ( 'NONE',  ( -61.00005817115211926, 195.0000036356967712, -0.1622090645192997005 ) ) ;
#11269=DIRECTION ( 'NONE',  ( -1.000000000000000000, 0.000000000000000000, 0.000000000000000000 ) ) ;
#11304=EDGE_LOOP ( 'NONE', ( #2341, #28612, #6308, #3584 ) ) ;
#11315=CIRCLE ( 'NONE', #2110, 5.200000000000002842 ) ;
#11411=EDGE_CURVE ( 'NONE', #33215, #13027, #32815, .T. ) ;
#11474=EDGE_CURVE ( 'NONE', #8568, #19176, #29336, .T. ) ;
#11477=VERTEX_POINT ( 'NONE', #24045 ) ;
#11492=CARTESIAN_POINT ( 'NONE',  ( -54.30000000000002558, -88.00000000000000000, -20.00000000000000000 ) ) ;
#11504=DIRECTION ( 'NONE',  ( -1.000000000000000000, 0.000000000000000000, 0.000000000000000000 ) ) ;
#11525=CARTESIAN_POINT ( 'NONE',  ( -60.00000000000000000, -7.347880794884118356E-15, -20.00000000000001776 ) ) ;
#11579=EDGE_LOOP ( 'NONE', ( #19660, #15278, #19292, #18626, #21013, #14385 ) ) ;
#11599=ORIENTED_EDGE ( 'NONE', *, *, #335, .T. ) ;
#11796=STYLED_ITEM ( 'NONE', ( #23501 ), #619 ) ;
#11881=EDGE_LOOP ( 'NONE', ( #15571, #15947, #28232, #29942 ) ) ;
#11941=DIRECTION ( 'NONE',  ( 0.000000000000000000, 0.000000000000000000, 1.000000000000000000 ) ) ;
#11993=DIRECTION ( 'NONE',  ( 0.000000000000000000, 0.000000000000000000, -1.000000000000000000 ) ) ;
#12048=ORIENTED_EDGE ( 'NONE', *, *, #15823, .T. ) ;
#12057=LINE ( 'NONE', #19563, #25977 ) ;
#12060=CARTESIAN_POINT ( 'NONE',  ( -67.50000000000000000, -92.00000000000000000, 270.4495957273638282 ) ) ;
#12138=ORIENTED_EDGE ( 'NONE', *, *, #12853, .F. ) ;
#12185=EDGE_CURVE ( 'NONE', #7112, #29388, #27985, .T. ) ;
#12190=DIRECTION ( 'NONE',  ( -1.000000000000000000, 0.000000000000000000, 0.000000000000000000 ) ) ;
#12214=ORIENTED_EDGE ( 'NONE', *, *, #22076, .T. ) ;
#12223=CARTESIAN_POINT ( 'NONE',  ( -58.50000000000002132, 209.9999999999999716, 0.000000000000000000 ) ) ;
#12246=CARTESIAN_POINT ( 'NONE',  ( -65.20000000000000284, -7.347880794884118356E-15, -19.30000000000003979 ) ) ;
#12303=FACE_OUTER_BOUND ( 'NONE', #23236, .T. ) ;
#12344=CARTESIAN_POINT ( 'NONE',  ( -67.50000000000000000, 155.0000000000000000, 6.938893903907228378E-15 ) ) ;
#12353=ORIENTED_EDGE ( 'NONE', *, *, #7308, .T. ) ;
#12354=CARTESIAN_POINT ( 'NONE',  ( -54.79999999999999716, -6.711064459327494323E-15, 270.4495957273638282 ) ) ;
#12383=CARTESIAN_POINT ( 'NONE',  ( -58.50000000000002132, 194.9217985566782829, -2.500000000000000000 ) ) ;
#12470=DIRECTION ( 'NONE',  ( 0.000000000000000000, 0.000000000000000000, -1.000000000000000000 ) ) ;
#12556=EDGE_LOOP ( 'NONE', ( #12734, #15904 ) ) ;
#12562=CARTESIAN_POINT ( 'NONE',  ( -56.61573505521625549, 194.9660755786677555, 1.651105572388385401 ) ) ;
#12598=CARTESIAN_POINT ( 'NONE',  ( -65.50384660342780307, 120.9385549553365706, 18.99615339657220758 ) ) ;
#12614=CARTESIAN_POINT ( 'NONE',  ( -58.50000000000002132, 209.9999999999999716, 0.000000000000000000 ) ) ;
#12626=CARTESIAN_POINT ( 'NONE',  ( 60.63708498984762940, 155.0000000000000000, 6.938893903907228378E-15 ) ) ;
#12655=EDGE_CURVE ( 'NONE', #14777, #4510, #26701, .T. ) ;
#12677=DIRECTION ( 'NONE',  ( 0.000000000000000000, 0.000000000000000000, -1.000000000000000000 ) ) ;
#12680=ORIENTED_EDGE ( 'NONE', *, *, #10368, .F. ) ;
#12684=ORIENTED_EDGE ( 'NONE', *, *, #14249, .F. ) ;
#12690=DIRECTION ( 'NONE',  ( 0.000000000000000000, 0.000000000000000000, 1.000000000000000000 ) ) ;
#12717=CARTESIAN_POINT ( 'NONE',  ( -64.96121601855533356, -1.809269760319439646, -19.53878398144470907 ) ) ;
#12718=VECTOR ( 'NONE', #33269, 1000.000000000000000 ) ;
#12734=ORIENTED_EDGE ( 'NONE', *, *, #858, .T. ) ;
#12737=CARTESIAN_POINT ( 'NONE',  ( -56.00013514549282689, 194.9999915534094725, -0.1669880218061202404 ) ) ;
#12779=SURFACE_STYLE_FILL_AREA ( #325 ) ;
#12843=ADVANCED_FACE ( 'NONE', ( #24514 ), #10910, .T. ) ;
#12853=EDGE_CURVE ( 'NONE', #8611, #16190, #21287, .T. ) ;
#12859=ORIENTED_EDGE ( 'NONE', *, *, #6440, .T. ) ;
#12900=CARTESIAN_POINT ( 'NONE',  ( -56.32919368135717519, 194.9806731544236982, 1.250698461946182505 ) ) ;
#12975=VERTEX_POINT ( 'NONE', #1849 ) ;
#13008=LINE ( 'NONE', #10122, #10226 ) ;
#13027=VERTEX_POINT ( 'NONE', #17180 ) ;
#13070=CARTESIAN_POINT ( 'NONE',  ( -56.97195197156149504, 194.9507991595696694, 1.985452284598899553 ) ) ;
#13164=DIRECTION ( 'NONE',  ( 0.000000000000000000, 0.000000000000000000, -1.000000000000000000 ) ) ;
#13181=AXIS2_PLACEMENT_3D ( 'NONE', #11525, #13406, #31637 ) ;
#13183=DIRECTION ( 'NONE',  ( 0.000000000000000000, 0.000000000000000000, -1.000000000000000000 ) ) ;
#13199=AXIS2_PLACEMENT_3D ( 'NONE', #15561, #23234, #10309 ) ;
#13269=EDGE_CURVE ( 'NONE', #250, #31739, #7332, .T. ) ;
#13342=VERTEX_POINT ( 'NONE', #16297 ) ;
#13390=CARTESIAN_POINT ( 'NONE',  ( 0.000000000000000000, 0.000000000000000000, -20.00000000000000000 ) ) ;
#13406=DIRECTION ( 'NONE',  ( 0.000000000000000000, 0.000000000000000000, -1.000000000000000000 ) ) ;
#13450=DIRECTION ( 'NONE',  ( 0.000000000000000000, -0.000000000000000000, -1.000000000000000000 ) ) ;
#13478=( BOUNDED_CURVE ( )  B_SPLINE_CURVE ( 3, ( #23736, #33464, #15565, #10313 ),
 .UNSPECIFIED., .F., .T. ) 
 B_SPLINE_CURVE_WITH_KNOTS ( ( 4, 4 ),
 ( 0.000000000000000000, 0.5248789335016748048 ),
 .UNSPECIFIED. ) 
 CURVE ( )  GEOMETRIC_REPRESENTATION_ITEM ( )  RATIONAL_B_SPLINE_CURVE ( ( 1.000000000000000000, 0.9771733092046011038, 0.9771733092046011038, 1.000000000000000000 ) ) 
 REPRESENTATION_ITEM ( '' )  );
#13505=FACE_OUTER_BOUND ( 'NONE', #11579, .T. ) ;
#13508=ORIENTED_EDGE ( 'NONE', *, *, #16605, .F. ) ;
#13542=EDGE_CURVE ( 'NONE', #25011, #12975, #19688, .T. ) ;
#13615=DIRECTION ( 'NONE',  ( -0.5773502691896268413, 0.5773502691896268413, -0.5773502691896235106 ) ) ;
#13707=CARTESIAN_POINT ( 'NONE',  ( -60.00000000000000000, -7.347880794884118356E-15, 270.4495957273638282 ) ) ;
#13735=VECTOR ( 'NONE', #21465, 1000.000000000000000 ) ;
#13776=AXIS2_PLACEMENT_3D ( 'NONE', #18597, #14310, #10932 ) ;
#13812=CARTESIAN_POINT ( 'NONE',  ( -59.14934243545564385, 194.9267577168561161, -2.419719764051426747 ) ) ;
#13827=AXIS2_PLACEMENT_3D ( 'NONE', #18576, #11230, #13450 ) ;
#13841=DIRECTION ( 'NONE',  ( -1.000000000000000000, 0.000000000000000000, 0.000000000000000000 ) ) ;
#13978=CARTESIAN_POINT ( 'NONE',  ( -59.30520453566667527, 194.9296309105606326, -2.372451168785852715 ) ) ;
#14018=EDGE_LOOP ( 'NONE', ( #31817, #12138, #20340, #23874, #18303, #29145, #1024 ) ) ;
#14022=EDGE_LOOP ( 'NONE', ( #25123, #1770, #12048, #29677 ) ) ;
#14061=VECTOR ( 'NONE', #15264, 1000.000000000000000 ) ;
#14067=CARTESIAN_POINT ( 'NONE',  ( -67.50000000000000000, 122.1366465496900275, 17.00000000000001421 ) ) ;
#14101=PLANE ( 'NONE',  #17318 ) ;
#14108=CARTESIAN_POINT ( 'NONE',  ( -54.79999999999999716, -6.711064459327494323E-15, -20.00000000000001776 ) ) ;
#14142=ORIENTED_EDGE ( 'NONE', *, *, #26799, .F. ) ;
#14147=DIRECTION ( 'NONE',  ( 0.000000000000000000, -1.000000000000000000, 0.000000000000000000 ) ) ;
#14173=VECTOR ( 'NONE', #13615, 1000.000000000000114 ) ;
#14175=CYLINDRICAL_SURFACE ( 'NONE', #5947, 17.00000000000000355 ) ;
#14209=DIRECTION ( 'NONE',  ( -1.000000000000000000, 0.000000000000000000, 0.000000000000000000 ) ) ;
#14249=EDGE_CURVE ( 'NONE', #15028, #5679, #1735, .T. ) ;
#14264=VECTOR ( 'NONE', #13841, 1000.000000000000000 ) ;
#14310=DIRECTION ( 'NONE',  ( 0.000000000000000000, 1.000000000000000000, 0.000000000000000000 ) ) ;
#14363=EDGE_CURVE ( 'NONE', #13342, #4045, #3388, .T. ) ;
#14373=EDGE_CURVE ( 'NONE', #25209, #8611, #31872, .T. ) ;
#14385=ORIENTED_EDGE ( 'NONE', *, *, #17675, .T. ) ;
#14386=FACE_OUTER_BOUND ( 'NONE', #21182, .T. ) ;
#14430=ORIENTED_EDGE ( 'NONE', *, *, #30538, .F. ) ;
#14435=ORIENTED_EDGE ( 'NONE', *, *, #12185, .F. ) ;
#14460=CARTESIAN_POINT ( 'NONE',  ( 60.63708498984762940, 120.3589838486224437, 20.00000000000000000 ) ) ;
#14468=AXIS2_PLACEMENT_3D ( 'NONE', #25147, #20210, #9480 ) ;
#14612=DIRECTION ( 'NONE',  ( 0.000000000000000000, 0.000000000000000000, 1.000000000000000000 ) ) ;
#14675=DIRECTION ( 'NONE',  ( -1.000000000000000000, -0.000000000000000000, -0.000000000000000000 ) ) ;
#14737=DIRECTION ( 'NONE',  ( 1.000000000000000000, 0.000000000000000000, 0.000000000000000000 ) ) ;
#14742=EDGE_CURVE ( 'NONE', #10143, #16190, #1766, .T. ) ;
#14749=DIRECTION ( 'NONE',  ( 0.000000000000000000, 0.000000000000000000, -1.000000000000000000 ) ) ;
#14777=VERTEX_POINT ( 'NONE', #472 ) ;
#14871=DIRECTION ( 'NONE',  ( 0.000000000000000000, -1.000000000000000000, 0.000000000000000000 ) ) ;
#14879=TOROIDAL_SURFACE ( 'NONE', #31214, 4.999999999999990230, 2.500000000000000000 ) ;
#14912=DIRECTION ( 'NONE',  ( 0.000000000000000000, 0.000000000000000000, 1.000000000000000000 ) ) ;
#14916=COLOUR_RGB ( '', 0.09019608, 0.27058824, 0.51372549) ;
#14941=MECHANICAL_DESIGN_GEOMETRIC_PRESENTATION_REPRESENTATION('',(#245),#20931);
#14997=CARTESIAN_POINT ( 'NONE',  ( -63.49999999999884892, 215.0000000000000000, -2.500000000000000000 ) ) ;
#15028=VERTEX_POINT ( 'NONE', #22079 ) ;
#15073=DIRECTION ( 'NONE',  ( 1.000000000000000000, 0.000000000000000000, -0.000000000000000000 ) ) ;
#15120=( LENGTH_UNIT ( ) NAMED_UNIT ( * ) SI_UNIT ( .MILLI., .METRE. ) );
#15167=PLANE ( 'NONE',  #4198 ) ;
#15247=PLANE ( 'NONE',  #4729 ) ;
#15264=DIRECTION ( 'NONE',  ( 0.000000000000000000, 1.000000000000000000, 0.000000000000000000 ) ) ;
#15278=ORIENTED_EDGE ( 'NONE', *, *, #26799, .T. ) ;
#15320=ORIENTED_EDGE ( 'NONE', *, *, #31577, .T. ) ;
#15470=CIRCLE ( 'NONE', #16551, 2.500000000000000000 ) ;
#15494=ORIENTED_EDGE ( 'NONE', *, *, #20197, .F. ) ;
#15500=FILL_AREA_STYLE_COLOUR ( '', #8001 ) ;
#15516=CYLINDRICAL_SURFACE ( 'NONE', #21098, 40.00000000000000711 ) ;
#15561=CARTESIAN_POINT ( 'NONE',  ( -64.50000000000000000, 155.0000000000000000, 6.938893903907228378E-15 ) ) ;
#15565=CARTESIAN_POINT ( 'NONE',  ( -64.96121601855533356, -1.809269760319447418, 19.53878398144468775 ) ) ;
#15571=ORIENTED_EDGE ( 'NONE', *, *, #17705, .F. ) ;
#15576=DIRECTION ( 'NONE',  ( 1.000000000000000000, 0.000000000000000000, 0.000000000000000000 ) ) ;
#15634=DIRECTION ( 'NONE',  ( 0.000000000000000000, 0.000000000000000000, -1.000000000000000000 ) ) ;
#15635=CARTESIAN_POINT ( 'NONE',  ( -64.50000000000000000, 155.0000000000000000, 6.938893903907228378E-15 ) ) ;
#15645=VECTOR ( 'NONE', #1662, 1000.000000000000000 ) ;
#15659=DIRECTION ( 'NONE',  ( -0.000000000000000000, -0.000000000000000000, -1.000000000000000000 ) ) ;
#15689=ORIENTED_EDGE ( 'NONE', *, *, #27696, .T. ) ;
#15715=DIRECTION ( 'NONE',  ( 0.000000000000000000, -1.000000000000000000, 0.000000000000000000 ) ) ;
#15739=AXIS2_PLACEMENT_3D ( 'NONE', #24181, #8836, #21618 ) ;
#15765=DIRECTION ( 'NONE',  ( 0.7071067811865454633, -0.000000000000000000, 0.7071067811865495711 ) ) ;
#15784=CARTESIAN_POINT ( 'NONE',  ( -56.33087447058203168, 194.9805812333615620, -1.253637678855320958 ) ) ;
#15791=ORIENTED_EDGE ( 'NONE', *, *, #17878, .T. ) ;
#15823=EDGE_CURVE ( 'NONE', #31739, #16522, #27877, .T. ) ;
#15867=ORIENTED_EDGE ( 'NONE', *, *, #26819, .F. ) ;
#15904=ORIENTED_EDGE ( 'NONE', *, *, #17705, .T. ) ;
#15936=ADVANCED_FACE ( 'NONE', ( #29512 ), #9406, .T. ) ;
#15947=ORIENTED_EDGE ( 'NONE', *, *, #32267, .T. ) ;
#15948=EDGE_CURVE ( 'NONE', #4045, #13342, #10552, .T. ) ;
#15957=ADVANCED_FACE ( 'NONE', ( #13505 ), #16062, .F. ) ;
#16005=EDGE_CURVE ( 'NONE', #2085, #4510, #3444, .T. ) ;
#16062=CYLINDRICAL_SURFACE ( 'NONE', #30677, 5.200000000000009948 ) ;
#16144=VECTOR ( 'NONE', #14147, 1000.000000000000000 ) ;
#16190=VERTEX_POINT ( 'NONE', #1728 ) ;
#16241=CIRCLE ( 'NONE', #7559, 2.500000000000000000 ) ;
#16297=CARTESIAN_POINT ( 'NONE',  ( -62.70000000000000284, -88.00000000000000000, 20.00000000000000000 ) ) ;
#16479=ORIENTED_EDGE ( 'NONE', *, *, #31409, .T. ) ;
#16522=VERTEX_POINT ( 'NONE', #33590 ) ;
#16531=CARTESIAN_POINT ( 'NONE',  ( -58.82891977373553516, 194.9228321189716837, -2.483646737656201253 ) ) ;
#16551=AXIS2_PLACEMENT_3D ( 'NONE', #12223, #9326, #30115 ) ;
#16588=ORIENTED_EDGE ( 'NONE', *, *, #9880, .T. ) ;
#16605=EDGE_CURVE ( 'NONE', #8327, #3502, #24610, .T. ) ;
#16619=CARTESIAN_POINT ( 'NONE',  ( -64.50000000000000000, 0.000000000000000000, 20.00000000000000000 ) ) ;
#16699=CARTESIAN_POINT ( 'NONE',  ( -60.38337337305365793, 194.9660334721754111, 1.652118058477962004 ) ) ;
#16839=UNCERTAINTY_MEASURE_WITH_UNIT (LENGTH_MEASURE( 1.000000000000000082E-05 ), #15120, 'distance_accuracy_value', 'NONE');
#16864=EDGE_LOOP ( 'NONE', ( #28444, #29506, #31890, #9287, #2255, #12684, #33603 ) ) ;
#16867=EDGE_LOOP ( 'NONE', ( #17031, #33400, #29649, #28398 ) ) ;
#16869=CARTESIAN_POINT ( 'NONE',  ( -60.87189664283175006, 194.9921494935721569, 0.8066102793772919055 ) ) ;
#16891=FACE_OUTER_BOUND ( 'NONE', #11304, .T. ) ;
#16998=CARTESIAN_POINT ( 'NONE',  ( -52.50000000000002132, -95.00000000000000000, 20.00000000000001776 ) ) ;
#17014=AXIS2_PLACEMENT_3D ( 'NONE', #2466, #28188, #12677 ) ;
#17031=ORIENTED_EDGE ( 'NONE', *, *, #29, .F. ) ;
#17041=ORIENTED_EDGE ( 'NONE', *, *, #11411, .F. ) ;
#17180=CARTESIAN_POINT ( 'NONE',  ( -58.50000000000002132, 209.9999999999999716, 2.500000000000000000 ) ) ;
#17218=AXIS2_PLACEMENT_3D ( 'NONE', #4973, #2084, #12470 ) ;
#17241=ADVANCED_FACE ( 'NONE', ( #8772 ), #21546, .F. ) ;
#17266=DIRECTION ( 'NONE',  ( -0.000000000000000000, -0.000000000000000000, -1.000000000000000000 ) ) ;
#17272=CARTESIAN_POINT ( 'NONE',  ( 60.63708498984762940, 155.0000000000000000, 6.938893903907228378E-15 ) ) ;
#17318=AXIS2_PLACEMENT_3D ( 'NONE', #32491, #29777, #27726 ) ;
#17327=CIRCLE ( 'NONE', #29832, 17.00000000000000711 ) ;
#17461=CARTESIAN_POINT ( 'NONE',  ( -67.50000000000000000, 155.0000000000000000, 6.938893903907228378E-15 ) ) ;
#17492=ORIENTED_EDGE ( 'NONE', *, *, #5854, .T. ) ;
#17499=AXIS2_PLACEMENT_3D ( 'NONE', #9638, #7093, #22081 ) ;
#17585=CARTESIAN_POINT ( 'NONE',  ( -63.50000000000001421, 210.0000000000000000, 0.000000000000000000 ) ) ;
#17634=DIRECTION ( 'NONE',  ( -1.000000000000000000, 0.000000000000000000, 0.000000000000000000 ) ) ;
#17636=FACE_OUTER_BOUND ( 'NONE', #7913, .T. ) ;
#17671=EDGE_CURVE ( 'NONE', #19176, #8611, #7069, .T. ) ;
#17675=EDGE_CURVE ( 'NONE', #5679, #8568, #13478, .T. ) ;
#17705=EDGE_CURVE ( 'NONE', #33308, #11477, #23006, .T. ) ;
#17769=AXIS2_PLACEMENT_3D ( 'NONE', #9673, #30123, #7467 ) ;
#17841=CARTESIAN_POINT ( 'NONE',  ( -58.16962743627800592, 194.9217985566782829, 2.500000000000000000 ) ) ;
#17850=( NAMED_UNIT ( * ) PLANE_ANGLE_UNIT ( ) SI_UNIT ( $, .RADIAN. ) );
#17878=EDGE_CURVE ( 'NONE', #28851, #2085, #2894, .T. ) ;
#17881=VERTEX_POINT ( 'NONE', #26295 ) ;
#17897=CARTESIAN_POINT ( 'NONE',  ( -64.50000000000000000, -95.00000000000000000, 270.4495957273638282 ) ) ;
#18056=LINE ( 'NONE', #18227, #922 ) ;
#18119=LINE ( 'NONE', #2116, #10216 ) ;
#18224=DIRECTION ( 'NONE',  ( 1.000000000000000000, 0.000000000000000000, 0.000000000000000000 ) ) ;
#18227=CARTESIAN_POINT ( 'NONE',  ( -67.50000000000000000, 155.0000000000000000, 37.00000000000001421 ) ) ;
#18303=ORIENTED_EDGE ( 'NONE', *, *, #12655, .T. ) ;
#18322=CARTESIAN_POINT ( 'NONE',  ( -67.50000000000000000, 0.000000000000000000, 270.4495957273638282 ) ) ;
#18356=AXIS2_PLACEMENT_3D ( 'NONE', #8419, #21353, #31588 ) ;
#18392=DIRECTION ( 'NONE',  ( 0.000000000000000000, -1.000000000000000000, 0.000000000000000000 ) ) ;
#18423=DIRECTION ( 'NONE',  ( -1.000000000000000000, 0.000000000000000000, 0.000000000000000000 ) ) ;
#18442=AXIS2_PLACEMENT_3D ( 'NONE', #18322, #20377, #20709 ) ;
#18475=FACE_BOUND ( 'NONE', #12556, .T. ) ;
#18505=SHAPE_REPRESENTATION ( 'pad arm left_left', ( #2404 ), #29608 ) ;
#18560=( NAMED_UNIT ( * ) PLANE_ANGLE_UNIT ( ) SI_UNIT ( $, .RADIAN. ) );
#18576=CARTESIAN_POINT ( 'NONE',  ( -125.0000000000000000, -95.00000000000000000, 270.4495957273638282 ) ) ;
#18577=CARTESIAN_POINT ( 'NONE',  ( -52.50000000000002132, 155.0000000000000000, 6.938893903907228378E-15 ) ) ;
#18597=CARTESIAN_POINT ( 'NONE',  ( -58.50000000000002132, 185.0000000000000000, 0.000000000000000000 ) ) ;
#18617=DIRECTION ( 'NONE',  ( 0.000000000000000000, 1.000000000000000000, 0.000000000000000000 ) ) ;
#18626=ORIENTED_EDGE ( 'NONE', *, *, #22085, .T. ) ;
#18636=ORIENTED_EDGE ( 'NONE', *, *, #21658, .F. ) ;
#18720=EDGE_CURVE ( 'NONE', #11477, #12975, #20521, .T. ) ;
#18767=LINE ( 'NONE', #3762, #16144 ) ;
#18842=UNCERTAINTY_MEASURE_WITH_UNIT (LENGTH_MEASURE( 1.000000000000000082E-05 ), #10239, 'distance_accuracy_value', 'NONE');
#18903=ADVANCED_FACE ( 'NONE', ( #18475, #26461 ), #25807, .T. ) ;
#18916=ORIENTED_EDGE ( 'NONE', *, *, #17671, .T. ) ;
#18921=DIRECTION ( 'NONE',  ( 1.000000000000000000, 0.000000000000000000, 0.000000000000000000 ) ) ;
#18927=CARTESIAN_POINT ( 'NONE',  ( -60.91988776943159678, 194.9950600780878460, 0.6490123436103525378 ) ) ;
#19046=ORIENTED_EDGE ( 'NONE', *, *, #9988, .T. ) ;
#19086=ORIENTED_EDGE ( 'NONE', *, *, #33029, .T. ) ;
#19094=CARTESIAN_POINT ( 'NONE',  ( -59.75243488385262225, 194.9412087183787037, 2.169815710172075196 ) ) ;
#19097=ORIENTED_EDGE ( 'NONE', *, *, #11474, .T. ) ;
#19176=VERTEX_POINT ( 'NONE', #25419 ) ;
#19240=CARTESIAN_POINT ( 'NONE',  ( -52.50000000000002132, 155.0000000000000000, 40.00000000000001421 ) ) ;
#19254=ORIENTED_EDGE ( 'NONE', *, *, #31577, .F. ) ;
#19292=ORIENTED_EDGE ( 'NONE', *, *, #14742, .T. ) ;
#19453=ADVANCED_FACE ( 'NONE', ( #12303 ), #14879, .T. ) ;
#19481=PRODUCT_DEFINITION_SHAPE ( 'NONE', 'NONE',  #6235 ) ;
#19518=FACE_OUTER_BOUND ( 'NONE', #16867, .T. ) ;
#19563=CARTESIAN_POINT ( 'NONE',  ( -52.50000000000002132, 0.000000000000000000, -20.00000000000000000 ) ) ;
#19590=ADVANCED_FACE ( 'NONE', ( #23381 ), #8211, .T. ) ;
#19660=ORIENTED_EDGE ( 'NONE', *, *, #25199, .F. ) ;
#19688=CIRCLE ( 'NONE', #17499, 17.00000000000000711 ) ;
#19745=CARTESIAN_POINT ( 'NONE',  ( -64.96121601855533356, 1.809269760319424769, -19.53878398144470907 ) ) ;
#19793=CYLINDRICAL_SURFACE ( 'NONE', #23865, 40.00000000000000711 ) ;
#20016=AXIS2_PLACEMENT_3D ( 'NONE', #17461, #17634, #5026 ) ;
#20058=CARTESIAN_POINT ( 'NONE',  ( -58.33685448808505214, 194.9217985566783113, -2.500000000000000444 ) ) ;
#20059=AXIS2_PLACEMENT_3D ( 'NONE', #1602, #29892, #11993 ) ;
#20067=( NAMED_UNIT ( * ) SI_UNIT ( $, .STERADIAN. ) SOLID_ANGLE_UNIT ( ) );
#20154=EDGE_CURVE ( 'NONE', #16522, #1291, #4456, .T. ) ;
#20197=EDGE_CURVE ( 'NONE', #31548, #10267, #21418, .T. ) ;
#20210=DIRECTION ( 'NONE',  ( 1.000000000000000000, 0.000000000000000000, 0.000000000000000000 ) ) ;
#20220=EDGE_LOOP ( 'NONE', ( #26878, #28937, #32318, #8326 ) ) ;
#20234=DIRECTION ( 'NONE',  ( 0.000000000000000000, 0.000000000000000000, -1.000000000000000000 ) ) ;
#20340=ORIENTED_EDGE ( 'NONE', *, *, #21993, .F. ) ;
#20365=DIRECTION ( 'NONE',  ( -0.000000000000000000, -0.000000000000000000, -1.000000000000000000 ) ) ;
#20369=CARTESIAN_POINT ( 'NONE',  ( -56.00000000000002132, 209.9999999999999716, 0.000000000000000000 ) ) ;
#20377=DIRECTION ( 'NONE',  ( -1.000000000000000000, 0.000000000000000000, 0.000000000000000000 ) ) ;
#20411=( NAMED_UNIT ( * ) PLANE_ANGLE_UNIT ( ) SI_UNIT ( $, .RADIAN. ) );
#20445=LINE ( 'NONE', #22997, #33023 ) ;
#20452=DIRECTION ( 'NONE',  ( -1.000000000000000000, 0.000000000000000000, 0.000000000000000000 ) ) ;
#20458=DIRECTION ( 'NONE',  ( 0.000000000000000000, 0.000000000000000000, -1.000000000000000000 ) ) ;
#20471=ORIENTED_EDGE ( 'NONE', *, *, #12853, .T. ) ;
#20501=CARTESIAN_POINT ( 'NONE',  ( -54.30000000000002558, -88.00000000000000000, 20.00000000000000000 ) ) ;
#20521=LINE ( 'NONE', #30415, #6136 ) ;
#20578=( LENGTH_UNIT ( ) NAMED_UNIT ( * ) SI_UNIT ( .MILLI., .METRE. ) );
#20616=CARTESIAN_POINT ( 'NONE',  ( -67.50000000000000000, 122.1366465496900275, 17.00000000000001421 ) ) ;
#20622=DIRECTION ( 'NONE',  ( 0.000000000000000000, 0.000000000000000000, -1.000000000000000000 ) ) ;
#20634=AXIS2_PLACEMENT_3D ( 'NONE', #24776, #14209, #32603 ) ;
#20635=FACE_BOUND ( 'NONE', #1821, .T. ) ;
#20641=AXIS2_PLACEMENT_3D ( 'NONE', #508, #20452, #13 ) ;
#20647=EDGE_CURVE ( 'NONE', #13027, #31548, #15470, .T. ) ;
#20709=DIRECTION ( 'NONE',  ( 0.000000000000000000, 0.000000000000000000, 1.000000000000000000 ) ) ;
#20749=CARTESIAN_POINT ( 'NONE',  ( -58.50000000000002132, 209.9999999999999716, 0.000000000000000000 ) ) ;
#20770=CARTESIAN_POINT ( 'NONE',  ( -52.50000000000002132, -95.00000000000000000, -20.00000000000000000 ) ) ;
#20779=CARTESIAN_POINT ( 'NONE',  ( -125.0000000000000000, -95.00000000000000000, 20.00000000000001776 ) ) ;
#20814=ORIENTED_EDGE ( 'NONE', *, *, #20647, .F. ) ;
#20858=EDGE_CURVE ( 'NONE', #23868, #17881, #26356, .T. ) ;
#20896=AXIS2_PLACEMENT_3D ( 'NONE', #33391, #2215, #18224 ) ;
#20907=CARTESIAN_POINT ( 'NONE',  ( -56.51026148866456111, 194.9712507328865740, 1.522362431316129916 ) ) ;
#20931=( GEOMETRIC_REPRESENTATION_CONTEXT ( 3 ) GLOBAL_UNCERTAINTY_ASSIGNED_CONTEXT ( ( #26095 ) ) GLOBAL_UNIT_ASSIGNED_CONTEXT ( ( #20578, #17850, #28414 ) ) REPRESENTATION_CONTEXT ( 'NONE', 'WORKASPACE' ) );
#20946=( NAMED_UNIT ( * ) SI_UNIT ( $, .STERADIAN. ) SOLID_ANGLE_UNIT ( ) );
#20950=FACE_OUTER_BOUND ( 'NONE', #28289, .T. ) ;
#21000=LINE ( 'NONE', #31398, #33287 ) ;
#21013=ORIENTED_EDGE ( 'NONE', *, *, #5854, .F. ) ;
#21028=DIRECTION ( 'NONE',  ( -0.000000000000000000, -0.000000000000000000, -1.000000000000000000 ) ) ;
#21055=ADVANCED_FACE ( 'NONE', ( #3965, #27472 ), #21067, .T. ) ;
#21067=PLANE ( 'NONE',  #21924 ) ;
#21098=AXIS2_PLACEMENT_3D ( 'NONE', #2753, #25, #345 ) ;
#21131=DIRECTION ( 'NONE',  ( 1.000000000000000000, 0.000000000000000000, 0.000000000000000000 ) ) ;
#21182=EDGE_LOOP ( 'NONE', ( #30617, #2803, #24705, #10325, #24243 ) ) ;
#21238=CARTESIAN_POINT ( 'NONE',  ( -64.50000000000000000, 155.0000000000000000, 40.00000000000001421 ) ) ;
#21287=LINE ( 'NONE', #29456, #31773 ) ;
#21353=DIRECTION ( 'NONE',  ( 1.000000000000000000, 0.000000000000000000, 0.000000000000000000 ) ) ;
#21403=AXIS2_PLACEMENT_3D ( 'NONE', #32454, #14912, #14737 ) ;
#21418=CIRCLE ( 'NONE', #20896, 2.499999999999988454 ) ;
#21465=DIRECTION ( 'NONE',  ( -1.000000000000000000, -0.000000000000000000, -0.000000000000000000 ) ) ;
#21483=CARTESIAN_POINT ( 'NONE',  ( -60.38481630464774241, 194.9660974499433053, -1.650668498912690740 ) ) ;
#21508=DIRECTION ( 'NONE',  ( 0.000000000000000000, 0.000000000000000000, 1.000000000000000000 ) ) ;
#21540=AXIS2_PLACEMENT_3D ( 'NONE', #30958, #28224, #33499 ) ;
#21546=CYLINDRICAL_SURFACE ( 'NONE', #7769, 5.200000000000009948 ) ;
#21618=DIRECTION ( 'NONE',  ( 0.000000000000000000, 0.000000000000000000, 1.000000000000000000 ) ) ;
#21651=DIRECTION ( 'NONE',  ( 1.000000000000000000, 0.000000000000000000, 0.000000000000000000 ) ) ;
#21658=EDGE_CURVE ( 'NONE', #15028, #27213, #23260, .T. ) ;
#21791=CARTESIAN_POINT ( 'NONE',  ( -52.50000000000002132, 155.0000000000000000, -16.99999999999999645 ) ) ;
#21924=AXIS2_PLACEMENT_3D ( 'NONE', #13390, #3802, #29693 ) ;
#21983=CARTESIAN_POINT ( 'NONE',  ( -59.75427847806285797, 194.9412682558892982, -2.168710897896606760 ) ) ;
#21993=EDGE_CURVE ( 'NONE', #31781, #8611, #18119, .T. ) ;
#22041=CARTESIAN_POINT ( 'NONE',  ( -60.00000000000000000, -7.347880794884118356E-15, 20.00000000000001776 ) ) ;
#22063=EDGE_LOOP ( 'NONE', ( #25447, #12353, #25932, #15867 ) ) ;
#22076=EDGE_CURVE ( 'NONE', #2474, #7112, #29164, .T. ) ;
#22079=CARTESIAN_POINT ( 'NONE',  ( -64.50000000000000000, 2.605762844159070557, 20.00000000000000000 ) ) ;
#22081=DIRECTION ( 'NONE',  ( 0.000000000000000000, 0.000000000000000000, -1.000000000000000000 ) ) ;
#22084=CARTESIAN_POINT ( 'NONE',  ( -54.50000000000002132, 155.0000000000000000, 6.938893903907228378E-15 ) ) ;
#22085=EDGE_CURVE ( 'NONE', #16190, #27924, #22630, .T. ) ;
#22098=ORIENTED_EDGE ( 'NONE', *, *, #32005, .T. ) ;
#22137=CONICAL_SURFACE ( 'NONE', #4183, 37.00000000000000711, 0.7853981633974482790 ) ;
#22177=AXIS2_PLACEMENT_3D ( 'NONE', #2740, #23505, #172 ) ;
#22180=AXIS2_PLACEMENT_3D ( 'NONE', #3247, #18921, #29146 ) ;
#22213=EDGE_LOOP ( 'NONE', ( #9914, #1368, #7287, #33293 ) ) ;
#22274=ADVANCED_FACE ( 'NONE', ( #25661 ), #30781, .T. ) ;
#22358=CARTESIAN_POINT ( 'NONE',  ( -52.50000000000002132, 120.3589838486224437, 20.00000000000000000 ) ) ;
#22378=FACE_OUTER_BOUND ( 'NONE', #4895, .T. ) ;
#22424=CARTESIAN_POINT ( 'NONE',  ( -65.20000000000000284, -7.347880794884118356E-15, -19.30000000000003979 ) ) ;
#22432=ORIENTED_EDGE ( 'NONE', *, *, #27883, .T. ) ;
#22448=DIRECTION ( 'NONE',  ( 0.000000000000000000, 0.000000000000000000, 1.000000000000000000 ) ) ;
#22468=LINE ( 'NONE', #14460, #10883 ) ;
#22516=DIRECTION ( 'NONE',  ( 0.000000000000000000, 0.000000000000000000, 1.000000000000000000 ) ) ;
#22552=CARTESIAN_POINT ( 'NONE',  ( -67.50000000000000000, 0.000000000000000000, 17.00000000000001421 ) ) ;
#22577=DIRECTION ( 'NONE',  ( 0.000000000000000000, 0.000000000000000000, -1.000000000000000000 ) ) ;
#22630=( BOUNDED_CURVE ( )  B_SPLINE_CURVE ( 3, ( #1644, #12717, #32983, #22424 ),
 .UNSPECIFIED., .F., .F. ) 
 B_SPLINE_CURVE_WITH_KNOTS ( ( 4, 4 ),
 ( 2.616713720088120532, 3.141592653589793116 ),
 .UNSPECIFIED. ) 
 CURVE ( )  GEOMETRIC_REPRESENTATION_ITEM ( )  RATIONAL_B_SPLINE_CURVE ( ( 1.000000000000000000, 0.9771733092046011038, 0.9771733092046011038, 1.000000000000000000 ) ) 
 REPRESENTATION_ITEM ( '' )  );
#22644=AXIS2_PLACEMENT_3D ( 'NONE', #22041, #17266, #27655 ) ;
#22680=CIRCLE ( 'NONE', #18356, 40.00000000000000711 ) ;
#22696=( GEOMETRIC_REPRESENTATION_CONTEXT ( 3 ) GLOBAL_UNCERTAINTY_ASSIGNED_CONTEXT ( ( #18842 ) ) GLOBAL_UNIT_ASSIGNED_CONTEXT ( ( #10239, #18560, #20946 ) ) REPRESENTATION_CONTEXT ( 'NONE', 'WORKASPACE' ) );
#22720=VECTOR ( 'NONE', #3014, 1000.000000000000000 ) ;
#22722=DIRECTION ( 'NONE',  ( 0.5773502691896268413, -0.5773502691896268413, -0.5773502691896235106 ) ) ;
#22833=EDGE_LOOP ( 'NONE', ( #26967, #31020, #4423, #23347 ) ) ;
#22906=ADVANCED_FACE ( 'NONE', ( #25411 ), #3069, .T. ) ;
#22970=DIRECTION ( 'NONE',  ( 0.000000000000000000, 0.000000000000000000, 1.000000000000000000 ) ) ;
#22997=CARTESIAN_POINT ( 'NONE',  ( -52.50000000000002132, 0.000000000000000000, 20.00000000000001776 ) ) ;
#23006=CIRCLE ( 'NONE', #27327, 17.00000000000000355 ) ;
#23029=AXIS2_PLACEMENT_3D ( 'NONE', #28666, #15715, #13164 ) ;
#23069=ORIENTED_EDGE ( 'NONE', *, *, #30538, .T. ) ;
#23120=ORIENTED_EDGE ( 'NONE', *, *, #227, .F. ) ;
#23126=CARTESIAN_POINT ( 'NONE',  ( -56.51255670714900248, 194.9711358487265613, -1.525379346234926992 ) ) ;
#23170=SURFACE_SIDE_STYLE ('',( #12779 ) ) ;
#23174=LINE ( 'NONE', #20779, #5830 ) ;
#23234=DIRECTION ( 'NONE',  ( 1.000000000000000000, 0.000000000000000000, 0.000000000000000000 ) ) ;
#23236=EDGE_LOOP ( 'NONE', ( #17041, #19086, #12214, #1116, #15494, #20814 ) ) ;
#23245=VECTOR ( 'NONE', #21028, 1000.000000000000000 ) ;
#23250=CARTESIAN_POINT ( 'NONE',  ( -65.20000000000000284, -7.347880794884118356E-15, 19.29999999999998295 ) ) ;
#23260=CIRCLE ( 'NONE', #22644, 5.200000000000002842 ) ;
#23347=ORIENTED_EDGE ( 'NONE', *, *, #16605, .T. ) ;
#23360=CARTESIAN_POINT ( 'NONE',  ( -63.49999999999884892, 215.0000000000003979, 0.000000000000000000 ) ) ;
#23362=FACE_OUTER_BOUND ( 'NONE', #24078, .T. ) ;
#23366=CARTESIAN_POINT ( 'NONE',  ( -63.50000000000004263, 215.0000000000000000, -2.500000000000000000 ) ) ;
#23381=FACE_OUTER_BOUND ( 'NONE', #28859, .T. ) ;
#23389=CARTESIAN_POINT ( 'NONE',  ( -64.96121601855533356, 1.809269760319432319, 19.53878398144468775 ) ) ;
#23393=CARTESIAN_POINT ( 'NONE',  ( -68.50000000000000000, 215.0000000000000000, -2.500000000000000000 ) ) ;
#23418=ORIENTED_EDGE ( 'NONE', *, *, #5625, .T. ) ;
#23423=CARTESIAN_POINT ( 'NONE',  ( -65.20000000000000284, -7.347880794884118356E-15, 270.4495957273638282 ) ) ;
#23460=CARTESIAN_POINT ( 'NONE',  ( -57.24471460971760450, 194.9412964752286825, 2.168227419017068502 ) ) ;
#23501=PRESENTATION_STYLE_ASSIGNMENT (( #2736 ) ) ;
#23505=DIRECTION ( 'NONE',  ( -1.000000000000000000, 0.000000000000000000, 0.000000000000000000 ) ) ;
#23518=CARTESIAN_POINT ( 'NONE',  ( -64.50000000000000000, 120.3589838486224579, -20.00000000000000000 ) ) ;
#23523=ADVANCED_FACE ( 'NONE', ( #10715 ), #5592, .T. ) ;
#23582=EDGE_LOOP ( 'NONE', ( #14142, #18636, #2682, #17492, #30500, #6940 ) ) ;
#23598=AXIS2_PLACEMENT_3D ( 'NONE', #6168, #10799, #24230 ) ;
#23633=LINE ( 'NONE', #26353, #22720 ) ;
#23663=CARTESIAN_POINT ( 'NONE',  ( -66.50402289005056389, 121.5305141831588003, 17.99597710994943967 ) ) ;
#23670=B_SPLINE_CURVE_WITH_KNOTS ( 'NONE', 3,
 ( #29481, #27262, #9034, #24543, #29656, #11104, #19094, #3416, #3586, #16699, #26587, #23870, #24034, #16869, #18927, #24205, #6305, #11263, #26753, #1041, #702, #26928, #32370, #868, #21483, #6490, #8704, #21983, #5971, #13978, #13812, #16531, #5800, #6137 ),
 .UNSPECIFIED., .F., .F.,
 ( 4, 2, 2, 2, 2, 2, 2, 2, 2, 2, 2, 2, 2, 2, 2, 2, 4 ),
 ( 0.000000000000000000, 0.0004886277888461246482, 0.0009772555776922492964, 0.001465883366538373945, 0.001954511155384498593, 0.002443138944230623458, 0.002931766733076747889, 0.003420394521922872320, 0.003909022310768997185, 0.004397650099615122050, 0.004886277888461246915, 0.005374905677307370913, 0.005863533466153495778, 0.006352161254999620643, 0.006840789043845744641, 0.007329416832691869506, 0.007818044621537994371 ),
 .UNSPECIFIED. ) ;
#23732=DIRECTION ( 'NONE',  ( 1.000000000000000000, 0.000000000000000000, 0.000000000000000000 ) ) ;
#23733=EDGE_LOOP ( 'NONE', ( #13508, #580 ) ) ;
#23736=CARTESIAN_POINT ( 'NONE',  ( -65.20000000000000284, -7.347880794884118356E-15, 19.29999999999998295 ) ) ;
#23865=AXIS2_PLACEMENT_3D ( 'NONE', #12626, #7363, #22516 ) ;
#23868=VERTEX_POINT ( 'NONE', #12383 ) ;
#23870=CARTESIAN_POINT ( 'NONE',  ( -60.66959905230670103, 194.9806057094332346, 1.252942659870247555 ) ) ;
#23874=ORIENTED_EDGE ( 'NONE', *, *, #335, .F. ) ;
#23882=DIRECTION ( 'NONE',  ( 0.000000000000000000, 0.000000000000000000, -1.000000000000000000 ) ) ;
#23899=DIRECTION ( 'NONE',  ( -1.000000000000000000, 0.000000000000000000, 0.000000000000000000 ) ) ;
#23912=ORIENTED_EDGE ( 'NONE', *, *, #30631, .T. ) ;
#24001=DIRECTION ( 'NONE',  ( -0.000000000000000000, -0.000000000000000000, -1.000000000000000000 ) ) ;
#24020=DIRECTION ( 'NONE',  ( 0.000000000000000000, 0.000000000000000000, -1.000000000000000000 ) ) ;
#24025=CARTESIAN_POINT ( 'NONE',  ( -58.50000000000001421, -88.00000000000000000, -20.00000000000000000 ) ) ;
#24034=CARTESIAN_POINT ( 'NONE',  ( -60.74722861894645831, 194.9849492171461804, 1.107464383744043657 ) ) ;
#24045=CARTESIAN_POINT ( 'NONE',  ( -52.50000000000002132, 155.0000000000000000, 17.00000000000001066 ) ) ;
#24078=EDGE_LOOP ( 'NONE', ( #15320, #28152, #32923, #28104 ) ) ;
#24079=LINE ( 'NONE', #6015, #23245 ) ;
#24103=AXIS2_PLACEMENT_3D ( 'NONE', #26410, #11240, #31849 ) ;
#24181=CARTESIAN_POINT ( 'NONE',  ( -52.50000000000002132, 155.0000000000000000, 6.938893903907228378E-15 ) ) ;
#24205=CARTESIAN_POINT ( 'NONE',  ( -60.98407617557292326, 194.9989950908677088, 0.3262505061364526227 ) ) ;
#24212=CARTESIAN_POINT ( 'NONE',  ( -52.50000000000002132, 120.3589838486224579, -20.00000000000000000 ) ) ;
#24230=DIRECTION ( 'NONE',  ( 1.000000000000000000, 0.000000000000000000, 0.000000000000000000 ) ) ;
#24243=ORIENTED_EDGE ( 'NONE', *, *, #7501, .T. ) ;
#24331=DIRECTION ( 'NONE',  ( -1.000000000000000000, 0.000000000000000000, 0.000000000000000000 ) ) ;
#24333=CIRCLE ( 'NONE', #22177, 37.00000000000000711 ) ;
#24379=ORIENTED_EDGE ( 'NONE', *, *, #9880, .F. ) ;
#24428=AXIS2_PLACEMENT_3D ( 'NONE', #28311, #21131, #10594 ) ;
#24506=FACE_OUTER_BOUND ( 'NONE', #22063, .T. ) ;
#24514=FACE_OUTER_BOUND ( 'NONE', #9603, .T. ) ;
#24543=CARTESIAN_POINT ( 'NONE',  ( -59.14727863148851839, 194.9267258542059835, 2.420242894197758510 ) ) ;
#24610=CIRCLE ( 'NONE', #27939, 4.199999999999988631 ) ;
#24624=ORIENTED_EDGE ( 'NONE', *, *, #11020, .T. ) ;
#24629=ORIENTED_EDGE ( 'NONE', *, *, #25199, .T. ) ;
#24640=VECTOR ( 'NONE', #31199, 1000.000000000000000 ) ;
#24660=ORIENTED_EDGE ( 'NONE', *, *, #20858, .F. ) ;
#24705=ORIENTED_EDGE ( 'NONE', *, *, #8477, .F. ) ;
#24776=CARTESIAN_POINT ( 'NONE',  ( -63.50000000000004263, 215.0000000000000000, 0.000000000000000000 ) ) ;
#24789=ADVANCED_FACE ( 'NONE', ( #8527 ), #10240, .T. ) ;
#24866=EDGE_LOOP ( 'NONE', ( #1700, #20471, #29911, #11175, #5669, #6951, #32444 ) ) ;
#25011=VERTEX_POINT ( 'NONE', #6814 ) ;
#25047=ORIENTED_EDGE ( 'NONE', *, *, #10771, .F. ) ;
#25069=DIRECTION ( 'NONE',  ( 0.000000000000000000, 0.000000000000000000, 1.000000000000000000 ) ) ;
#25081=VERTEX_POINT ( 'NONE', #1192 ) ;
#25115=DIRECTION ( 'NONE',  ( -1.000000000000000000, 0.000000000000000000, 0.000000000000000000 ) ) ;
#25123=ORIENTED_EDGE ( 'NONE', *, *, #5370, .T. ) ;
#25147=CARTESIAN_POINT ( 'NONE',  ( -63.49999999999884892, 215.0000000000003979, 0.000000000000000000 ) ) ;
#25160=ORIENTED_EDGE ( 'NONE', *, *, #17671, .F. ) ;
#25167=CARTESIAN_POINT ( 'NONE',  ( -52.50000000000002132, 155.0000000000000000, 6.938893903907228378E-15 ) ) ;
#25199=EDGE_CURVE ( 'NONE', #27213, #8568, #11315, .T. ) ;
#25209=VERTEX_POINT ( 'NONE', #20770 ) ;
#25371=ORIENTED_EDGE ( 'NONE', *, *, #4985, .T. ) ;
#25372=AXIS2_PLACEMENT_3D ( 'NONE', #12344, #25115, #27836 ) ;
#25406=ORIENTED_EDGE ( 'NONE', *, *, #26845, .T. ) ;
#25411=FACE_OUTER_BOUND ( 'NONE', #20220, .T. ) ;
#25419=CARTESIAN_POINT ( 'NONE',  ( -64.50000000000000000, -95.00000000000000000, 20.00000000000001776 ) ) ;
#25427=CARTESIAN_POINT ( 'NONE',  ( -64.50000000000000000, 2.605762844159070557, 20.00000000000000000 ) ) ;
#25447=ORIENTED_EDGE ( 'NONE', *, *, #14363, .T. ) ;
#25508=CARTESIAN_POINT ( 'NONE',  ( -57.24307706584514932, 194.9404480003898925, -2.185445380844633689 ) ) ;
#25551=CARTESIAN_POINT ( 'NONE',  ( -64.50000000000000000, 120.3589838486224437, 20.00000000000000000 ) ) ;
#25630=ADVANCED_FACE ( 'NONE', ( #32997 ), #14101, .F. ) ;
#25639=ORIENTED_EDGE ( 'NONE', *, *, #637, .F. ) ;
#25661=FACE_OUTER_BOUND ( 'NONE', #27875, .T. ) ;
#25678=CARTESIAN_POINT ( 'NONE',  ( -55.99986651211894184, 195.0000083429897586, 0.1629166443388770646 ) ) ;
#25685=CARTESIAN_POINT ( 'NONE',  ( -61.00000000000002842, 209.9999999999999716, -3.061616997868380183E-16 ) ) ;
#25807=PLANE ( 'NONE',  #2926 ) ;
#25827=FACE_OUTER_BOUND ( 'NONE', #3239, .T. ) ;
#25895=DIRECTION ( 'NONE',  ( 0.7071067811865475727, 0.7071067811865475727, 0.000000000000000000 ) ) ;
#25915=ORIENTED_EDGE ( 'NONE', *, *, #13542, .F. ) ;
#25932=ORIENTED_EDGE ( 'NONE', *, *, #33085, .T. ) ;
#25951=VERTEX_POINT ( 'NONE', #7294 ) ;
#25977=VECTOR ( 'NONE', #6782, 1000.000000000000000 ) ;
#25983=AXIS2_PLACEMENT_3D ( 'NONE', #25167, #6607, #14612 ) ;
#26059=DIRECTION ( 'NONE',  ( 1.000000000000000000, 0.000000000000000000, 0.000000000000000000 ) ) ;
#26072=CARTESIAN_POINT ( 'NONE',  ( -63.49999999999884892, 217.5000000000001990, 0.000000000000000000 ) ) ;
#26089=CARTESIAN_POINT ( 'NONE',  ( -64.50000000000000000, -2.605762844159085212, 20.00000000000000000 ) ) ;
#26095=UNCERTAINTY_MEASURE_WITH_UNIT (LENGTH_MEASURE( 1.000000000000000082E-05 ), #20578, 'distance_accuracy_value', 'NONE');
#26153=CIRCLE ( 'NONE', #642, 2.500000000000000000 ) ;
#26160=DIRECTION ( 'NONE',  ( 0.000000000000000000, 1.000000000000000000, 0.000000000000000000 ) ) ;
#26177=CARTESIAN_POINT ( 'NONE',  ( -57.85233474027615586, 194.9267265987278961, -2.420233332361308332 ) ) ;
#26231=VECTOR ( 'NONE', #11269, 1000.000000000000000 ) ;
#26295=CARTESIAN_POINT ( 'NONE',  ( -58.50000000000002132, 194.9217985566782829, 2.500000000000000000 ) ) ;
#26353=CARTESIAN_POINT ( 'NONE',  ( -52.50000000000002132, -95.00000000000000000, 270.4495957273638282 ) ) ;
#26356=B_SPLINE_CURVE_WITH_KNOTS ( 'NONE', 3,
 ( #9666, #20058, #30797, #26177, #7634, #25508, #10362, #4898, #23126, #15784, #125, #2178, #2692, #33514, #12737, #25678, #28580, #2845, #7459, #30627, #12900, #20907, #12562, #2347, #13070, #23460, #10528, #31303, #17841, #31132 ),
 .UNSPECIFIED., .F., .F.,
 ( 4, 2, 2, 2, 2, 2, 2, 2, 2, 2, 2, 2, 2, 2, 4 ),
 ( 0.007818044621537994371, 0.008306560441632113850, 0.008795076261726231595, 0.009772107901914449737, 0.01026062372200855187, 0.01074913954210265227, 0.01123765536219675440, 0.01172617118229085653, 0.01221468700238495693, 0.01270320282247905906, 0.01319171864257315946, 0.01368023446266726159, 0.01416875028276136372, 0.01465726610285546412, 0.01563429774304366665 ),
 .UNSPECIFIED. ) ;
#26410=CARTESIAN_POINT ( 'NONE',  ( -58.50000000000001421, -88.00000000000000000, -20.00000000000000000 ) ) ;
#26461=FACE_OUTER_BOUND ( 'NONE', #10975, .T. ) ;
#26566=ADVANCED_FACE ( 'NONE', ( #19518 ), #22137, .T. ) ;
#26587=CARTESIAN_POINT ( 'NONE',  ( -60.48684543773389066, 194.9711049089068808, 1.526260319620769579 ) ) ;
#26600=EDGE_CURVE ( 'NONE', #11107, #250, #5028, .T. ) ;
#26630=ADVANCED_FACE ( 'NONE', ( #32962, #17636 ), #15247, .T. ) ;
#26683=CIRCLE ( 'NONE', #9676, 40.00000000000000711 ) ;
#26701=B_SPLINE_CURVE_WITH_KNOTS ( 'NONE', 3,
 ( #4784, #33577, #10256, #23518 ),
 .UNSPECIFIED., .F., .F.,
 ( 4, 4 ),
 ( 0.000000000000000000, 0.004600009204204574646 ),
 .UNSPECIFIED. ) ;
#26753=CARTESIAN_POINT ( 'NONE',  ( -60.98379214578430663, 194.9989775857802385, -0.3278793750673599239 ) ) ;
#26787=EDGE_LOOP ( 'NONE', ( #30886, #10484 ) ) ;
#26799=EDGE_CURVE ( 'NONE', #27213, #10143, #33646, .T. ) ;
#26819=EDGE_CURVE ( 'NONE', #13342, #8327, #24079, .T. ) ;
#26845=EDGE_CURVE ( 'NONE', #4510, #250, #22680, .T. ) ;
#26878=ORIENTED_EDGE ( 'NONE', *, *, #590, .F. ) ;
#26928=CARTESIAN_POINT ( 'NONE',  ( -60.74744875717816939, 194.9849611312037041, -1.107162489773501513 ) ) ;
#26967=ORIENTED_EDGE ( 'NONE', *, *, #7308, .F. ) ;
#26999=AXIS2_PLACEMENT_3D ( 'NONE', #33359, #32840, #20234 ) ;
#27213=VERTEX_POINT ( 'NONE', #31595 ) ;
#27226=CARTESIAN_POINT ( 'NONE',  ( -60.00000000000000000, -7.347880794884118356E-15, -20.00000000000001776 ) ) ;
#27262=CARTESIAN_POINT ( 'NONE',  ( -58.66522414286995968, 194.9217985566782545, 2.500000000000000444 ) ) ;
#27327=AXIS2_PLACEMENT_3D ( 'NONE', #402, #10135, #10639 ) ;
#27349=CARTESIAN_POINT ( 'NONE',  ( -58.50000000000001421, -88.00000000000000000, -20.00000000000000000 ) ) ;
#27472=FACE_OUTER_BOUND ( 'NONE', #24866, .T. ) ;
#27554=DIRECTION ( 'NONE',  ( -1.000000000000000000, 0.000000000000000000, 0.000000000000000000 ) ) ;
#27655=DIRECTION ( 'NONE',  ( 1.000000000000000000, 0.000000000000000000, 0.000000000000000000 ) ) ;
#27661=DIRECTION ( 'NONE',  ( 0.000000000000000000, 0.000000000000000000, 1.000000000000000000 ) ) ;
#27677=SHAPE_REPRESENTATION_RELATIONSHIP ( 'NONE' , 'NONE' ,  #18505, #10045 ) ;
#27696=EDGE_CURVE ( 'NONE', #25951, #1291, #30391, .T. ) ;
#27726=DIRECTION ( 'NONE',  ( 0.000000000000000000, 1.000000000000000000, -0.000000000000000000 ) ) ;
#27836=DIRECTION ( 'NONE',  ( 0.000000000000000000, 0.000000000000000000, 1.000000000000000000 ) ) ;
#27840=ORIENTED_EDGE ( 'NONE', *, *, #7501, .F. ) ;
#27875=EDGE_LOOP ( 'NONE', ( #32362, #25915 ) ) ;
#27877=CIRCLE ( 'NONE', #13199, 40.00000000000000711 ) ;
#27883=EDGE_CURVE ( 'NONE', #23868, #32869, #13008, .T. ) ;
#27893=CARTESIAN_POINT ( 'NONE',  ( -63.49999999999884892, 212.5000000000003695, -3.061616997868142046E-16 ) ) ;
#27924=VERTEX_POINT ( 'NONE', #31074 ) ;
#27939=AXIS2_PLACEMENT_3D ( 'NONE', #24025, #688, #18423 ) ;
#27985=LINE ( 'NONE', #28160, #12718 ) ;
#28059=ORIENTED_EDGE ( 'NONE', *, *, #3127, .F. ) ;
#28104=ORIENTED_EDGE ( 'NONE', *, *, #945, .F. ) ;
#28152=ORIENTED_EDGE ( 'NONE', *, *, #32280, .T. ) ;
#28160=CARTESIAN_POINT ( 'NONE',  ( -63.50000000000004263, 215.0000000000000000, 2.500000000000000000 ) ) ;
#28188=DIRECTION ( 'NONE',  ( -1.000000000000000000, -0.000000000000000000, 0.000000000000000000 ) ) ;
#28224=DIRECTION ( 'NONE',  ( 1.000000000000000000, 0.000000000000000000, -0.000000000000000000 ) ) ;
#28232=ORIENTED_EDGE ( 'NONE', *, *, #13542, .T. ) ;
#28260=DIRECTION ( 'NONE',  ( 1.000000000000000000, 0.000000000000000000, 0.000000000000000000 ) ) ;
#28289=EDGE_LOOP ( 'NONE', ( #6601, #28059, #2344, #25160 ) ) ;
#28311=CARTESIAN_POINT ( 'NONE',  ( -68.50000000000000000, 215.0000000000000000, 0.000000000000000000 ) ) ;
#28364=DIRECTION ( 'NONE',  ( -1.000000000000000000, -0.000000000000000000, -0.000000000000000000 ) ) ;
#28398=ORIENTED_EDGE ( 'NONE', *, *, #12655, .F. ) ;
#28414=( NAMED_UNIT ( * ) SI_UNIT ( $, .STERADIAN. ) SOLID_ANGLE_UNIT ( ) );
#28444=ORIENTED_EDGE ( 'NONE', *, *, #20154, .T. ) ;
#28509=PLANE ( 'NONE',  #7250 ) ;
#28536=CARTESIAN_POINT ( 'NONE',  ( -52.50000000000002132, 0.000000000000000000, 270.4495957273638282 ) ) ;
#28563=ADVANCED_FACE ( 'NONE', ( #20635, #23362 ), #15516, .T. ) ;
#28580=CARTESIAN_POINT ( 'NONE',  ( -56.01598787314604522, 194.9989914758641305, 0.3258944654411097264 ) ) ;
#28590=CARTESIAN_POINT ( 'NONE',  ( -54.30000000000001847, -88.00000000000000000, -20.00000000000000000 ) ) ;
#28612=ORIENTED_EDGE ( 'NONE', *, *, #858, .F. ) ;
#28666=CARTESIAN_POINT ( 'NONE',  ( -58.50000000000002132, 209.9999999999999716, 0.000000000000000000 ) ) ;
#28786=APPLICATION_CONTEXT ( 'automotive_design' ) ;
#28851=VERTEX_POINT ( 'NONE', #11233 ) ;
#28859=EDGE_LOOP ( 'NONE', ( #24660, #22432, #23912, #5304, #428 ) ) ;
#28882=FACE_OUTER_BOUND ( 'NONE', #14018, .T. ) ;
#28898=VERTEX_POINT ( 'NONE', #19240 ) ;
#28937=ORIENTED_EDGE ( 'NONE', *, *, #5625, .F. ) ;
#28961=DIRECTION ( 'NONE',  ( 0.000000000000000000, 2.081668171172168119E-15, -1.000000000000000000 ) ) ;
#28998=FACE_OUTER_BOUND ( 'NONE', #29696, .T. ) ;
#29031=LINE ( 'NONE', #23423, #968 ) ;
#29133=CYLINDRICAL_SURFACE ( 'NONE', #24103, 4.199999999999988631 ) ;
#29145=ORIENTED_EDGE ( 'NONE', *, *, #29910, .F. ) ;
#29146=DIRECTION ( 'NONE',  ( 0.000000000000000000, 0.000000000000000000, -1.000000000000000000 ) ) ;
#29164=CIRCLE ( 'NONE', #14468, 2.500000000000000000 ) ;
#29181=ORIENTED_EDGE ( 'NONE', *, *, #4153, .T. ) ;
#29190=CLOSED_SHELL ( 'NONE', ( #19453, #2764, #2518, #19590, #5351, #24789, #26566, #15957, #28563, #30222, #7530, #6903, #12843, #18903, #17241, #21055, #26630, #22906, #25630, #30151, #9957, #8107, #7335, #15936, #23523, #11211, #32168, #22274 ) ) ;
#29336=LINE ( 'NONE', #32382, #30097 ) ;
#29388=VERTEX_POINT ( 'NONE', #8799 ) ;
#29430=ORIENTED_EDGE ( 'NONE', *, *, #16005, .T. ) ;
#29456=CARTESIAN_POINT ( 'NONE',  ( -64.50000000000000000, 0.000000000000000000, -20.00000000000000000 ) ) ;
#29481=CARTESIAN_POINT ( 'NONE',  ( -58.50000000000002132, 194.9217985566782829, 2.500000000000000000 ) ) ;
#29506=ORIENTED_EDGE ( 'NONE', *, *, #27696, .F. ) ;
#29512=FACE_OUTER_BOUND ( 'NONE', #6810, .T. ) ;
#29596=EDGE_CURVE ( 'NONE', #12975, #25011, #17327, .T. ) ;
#29608=( GEOMETRIC_REPRESENTATION_CONTEXT ( 3 ) GLOBAL_UNCERTAINTY_ASSIGNED_CONTEXT ( ( #16839 ) ) GLOBAL_UNIT_ASSIGNED_CONTEXT ( ( #15120, #20411, #20067 ) ) REPRESENTATION_CONTEXT ( 'NONE', 'WORKASPACE' ) );
#29609=ORIENTED_EDGE ( 'NONE', *, *, #29, .T. ) ;
#29649=ORIENTED_EDGE ( 'NONE', *, *, #26845, .F. ) ;
#29656=CARTESIAN_POINT ( 'NONE',  ( -59.30608239026425821, 194.9296489543815483, 2.372148111071822996 ) ) ;
#29677=ORIENTED_EDGE ( 'NONE', *, *, #8738, .T. ) ;
#29693=DIRECTION ( 'NONE',  ( -1.000000000000000000, 0.000000000000000000, -0.000000000000000000 ) ) ;
#29696=EDGE_LOOP ( 'NONE', ( #27840, #14430 ) ) ;
#29727=CIRCLE ( 'NONE', #26999, 40.00000000000000711 ) ;
#29777=DIRECTION ( 'NONE',  ( 0.7071067811865454633, -0.000000000000000000, -0.7071067811865495711 ) ) ;
#29832=AXIS2_PLACEMENT_3D ( 'NONE', #22084, #9138, #14749 ) ;
#29853=ORIENTED_EDGE ( 'NONE', *, *, #21658, .T. ) ;
#29883=AXIS2_PLACEMENT_3D ( 'NONE', #12614, #10080, #20458 ) ;
#29892=DIRECTION ( 'NONE',  ( 1.000000000000000000, 0.000000000000000000, 0.000000000000000000 ) ) ;
#29910=EDGE_CURVE ( 'NONE', #25081, #4510, #4875, .T. ) ;
#29911=ORIENTED_EDGE ( 'NONE', *, *, #14742, .F. ) ;
#29942=ORIENTED_EDGE ( 'NONE', *, *, #18720, .F. ) ;
#30097=VECTOR ( 'NONE', #3597, 1000.000000000000000 ) ;
#30115=DIRECTION ( 'NONE',  ( 0.000000000000000000, 0.000000000000000000, -1.000000000000000000 ) ) ;
#30117=CARTESIAN_POINT ( 'NONE',  ( 60.63708498984762940, 155.0000000000000000, 40.00000000000001421 ) ) ;
#30123=DIRECTION ( 'NONE',  ( 1.000000000000000000, 0.000000000000000000, 0.000000000000000000 ) ) ;
#30151=ADVANCED_FACE ( 'NONE', ( #28882 ), #2991, .F. ) ;
#30222=ADVANCED_FACE ( 'NONE', ( #32728 ), #19793, .T. ) ;
#30231=ORIENTED_EDGE ( 'NONE', *, *, #22076, .F. ) ;
#30325=CIRCLE ( 'NONE', #30904, 5.200000000000009948 ) ;
#30391=LINE ( 'NONE', #22552, #4759 ) ;
#30415=CARTESIAN_POINT ( 'NONE',  ( -52.50000000000002132, 155.0000000000000000, 17.00000000000001066 ) ) ;
#30464=FILL_AREA_STYLE ('',( #7124 ) ) ;
#30495=ORIENTED_EDGE ( 'NONE', *, *, #14373, .F. ) ;
#30500=ORIENTED_EDGE ( 'NONE', *, *, #32635, .T. ) ;
#30538=EDGE_CURVE ( 'NONE', #30979, #29388, #8126, .T. ) ;
#30617=ORIENTED_EDGE ( 'NONE', *, *, #32005, .F. ) ;
#30627=CARTESIAN_POINT ( 'NONE',  ( -56.25248981486732447, 194.9849645003486387, 1.107065583161625621 ) ) ;
#30631=EDGE_CURVE ( 'NONE', #32869, #33215, #6485, .T. ) ;
#30677=AXIS2_PLACEMENT_3D ( 'NONE', #31894, #1071, #23899 ) ;
#30781=PLANE ( 'NONE',  #21540 ) ;
#30797=CARTESIAN_POINT ( 'NONE',  ( -58.17468396801123731, 194.9227987135369062, -2.484183799773476142 ) ) ;
#30804=SURFACE_STYLE_USAGE ( .BOTH. , #33358 ) ;
#30858=SHAPE_DEFINITION_REPRESENTATION ( #19481, #18505 ) ;
#30886=ORIENTED_EDGE ( 'NONE', *, *, #14363, .F. ) ;
#30899=CARTESIAN_POINT ( 'NONE',  ( -67.50000000000000000, 155.0000000000000000, -37.00000000000000000 ) ) ;
#30904=AXIS2_PLACEMENT_3D ( 'NONE', #27226, #7123, #27554 ) ;
#30958=CARTESIAN_POINT ( 'NONE',  ( -54.50000000000002132, 0.000000000000000000, 270.4495957273638282 ) ) ;
#30979=VERTEX_POINT ( 'NONE', #23393 ) ;
#31020=ORIENTED_EDGE ( 'NONE', *, *, #15948, .T. ) ;
#31074=CARTESIAN_POINT ( 'NONE',  ( -65.20000000000000284, -7.347880794884118356E-15, -19.30000000000003979 ) ) ;
#31132=CARTESIAN_POINT ( 'NONE',  ( -58.50000000000002132, 194.9217985566782829, 2.500000000000000000 ) ) ;
#31199=DIRECTION ( 'NONE',  ( -1.000000000000000000, 0.000000000000000000, 0.000000000000000000 ) ) ;
#31200=AXIS2_PLACEMENT_3D ( 'NONE', #27349, #4015, #12190 ) ;
#31214=AXIS2_PLACEMENT_3D ( 'NONE', #17585, #33259, #9925 ) ;
#31294=VERTEX_POINT ( 'NONE', #16998 ) ;
#31303=CARTESIAN_POINT ( 'NONE',  ( -57.84141927132884575, 194.9260988872778171, 2.433575273292319707 ) ) ;
#31364=CIRCLE ( 'NONE', #25372, 37.00000000000000711 ) ;
#31398=CARTESIAN_POINT ( 'NONE',  ( -58.50000000000002132, 185.0000000000000000, 2.500000000000000000 ) ) ;
#31409=EDGE_CURVE ( 'NONE', #10267, #2381, #4704, .T. ) ;
#31455=CIRCLE ( 'NONE', #20016, 37.00000000000000711 ) ;
#31513=FACE_OUTER_BOUND ( 'NONE', #31763, .T. ) ;
#31522=DIRECTION ( 'NONE',  ( 0.000000000000000000, 0.000000000000000000, -1.000000000000000000 ) ) ;
#31548=VERTEX_POINT ( 'NONE', #25685 ) ;
#31556=CARTESIAN_POINT ( 'NONE',  ( -68.50000000000000000, 215.0000000000000000, 0.000000000000000000 ) ) ;
#31577=EDGE_CURVE ( 'NONE', #28898, #28851, #29727, .T. ) ;
#31588=DIRECTION ( 'NONE',  ( 0.000000000000000000, 0.000000000000000000, 1.000000000000000000 ) ) ;
#31595=CARTESIAN_POINT ( 'NONE',  ( -54.79999999999999716, -6.711064459327494323E-15, 20.00000000000001776 ) ) ;
#31616=APPLICATION_CONTEXT ( 'automotive_design' ) ;
#31637=DIRECTION ( 'NONE',  ( -1.000000000000000000, 0.000000000000000000, 0.000000000000000000 ) ) ;
#31682=FACE_OUTER_BOUND ( 'NONE', #11881, .T. ) ;
#31732=CARTESIAN_POINT ( 'NONE',  ( -63.50000000000001421, 210.0000000000000000, 0.000000000000000000 ) ) ;
#31739=VERTEX_POINT ( 'NONE', #21238 ) ;
#31763=EDGE_LOOP ( 'NONE', ( #10355, #22098, #23069, #14435, #30231 ) ) ;
#31773=VECTOR ( 'NONE', #6107, 1000.000000000000000 ) ;
#31781=VERTEX_POINT ( 'NONE', #10863 ) ;
#31817=ORIENTED_EDGE ( 'NONE', *, *, #22085, .F. ) ;
#31849=DIRECTION ( 'NONE',  ( -1.000000000000000000, 0.000000000000000000, 0.000000000000000000 ) ) ;
#31872=LINE ( 'NONE', #8709, #26231 ) ;
#31890=ORIENTED_EDGE ( 'NONE', *, *, #5218, .F. ) ;
#31894=CARTESIAN_POINT ( 'NONE',  ( -60.00000000000000000, -7.347880794884118356E-15, 270.4495957273638282 ) ) ;
#31908=DIRECTION ( 'NONE',  ( -0.000000000000000000, -0.000000000000000000, -1.000000000000000000 ) ) ;
#31987=VERTEX_POINT ( 'NONE', #5465 ) ;
#32005=EDGE_CURVE ( 'NONE', #2381, #30979, #9910, .T. ) ;
#32012=DIRECTION ( 'NONE',  ( -1.000000000000000000, -0.000000000000000000, 0.000000000000000000 ) ) ;
#32019=LINE ( 'NONE', #32183, #165 ) ;
#32035=AXIS2_PLACEMENT_3D ( 'NONE', #9058, #15765, #26160 ) ;
#32125=AXIS2_PLACEMENT_3D ( 'NONE', #5934, #24001, #24331 ) ;
#32168=ADVANCED_FACE ( 'NONE', ( #1019 ), #29133, .F. ) ;
#32183=CARTESIAN_POINT ( 'NONE',  ( 60.63708498984762940, 155.0000000000000000, -40.00000000000000000 ) ) ;
#32199=ORIENTED_EDGE ( 'NONE', *, *, #3127, .T. ) ;
#32246=ORIENTED_EDGE ( 'NONE', *, *, #10771, .T. ) ;
#32267=EDGE_CURVE ( 'NONE', #33308, #25011, #8513, .T. ) ;
#32277=DIRECTION ( 'NONE',  ( -0.000000000000000000, -0.000000000000000000, -1.000000000000000000 ) ) ;
#32280=EDGE_CURVE ( 'NONE', #28851, #250, #32019, .T. ) ;
#32318=ORIENTED_EDGE ( 'NONE', *, *, #20154, .F. ) ;
#32337=CYLINDRICAL_SURFACE ( 'NONE', #32125, 4.199999999999988631 ) ;
#32352=CARTESIAN_POINT ( 'NONE',  ( -65.20000000000000284, 0.9203920079924583497, -19.30000000000004690 ) ) ;
#32353=DIRECTION ( 'NONE',  ( 1.000000000000000000, -0.000000000000000000, -0.000000000000000000 ) ) ;
#32362=ORIENTED_EDGE ( 'NONE', *, *, #29596, .F. ) ;
#32370=CARTESIAN_POINT ( 'NONE',  ( -60.66914996032592455, 194.9805833264304908, -1.253524243223063994 ) ) ;
#32382=CARTESIAN_POINT ( 'NONE',  ( -64.50000000000000000, 0.000000000000000000, 20.00000000000000000 ) ) ;
#32444=ORIENTED_EDGE ( 'NONE', *, *, #10368, .T. ) ;
#32454=CARTESIAN_POINT ( 'NONE',  ( -63.50000000000001421, 210.0000000000000000, 0.000000000000000000 ) ) ;
#32491=CARTESIAN_POINT ( 'NONE',  ( -67.50000000000000000, 0.000000000000000000, 17.00000000000001421 ) ) ;
#32603=DIRECTION ( 'NONE',  ( 0.000000000000000000, 0.000000000000000000, 1.000000000000000000 ) ) ;
#32635=EDGE_CURVE ( 'NONE', #27924, #25081, #9136, .T. ) ;
#32728=FACE_OUTER_BOUND ( 'NONE', #14022, .T. ) ;
#32791=AXIS2_PLACEMENT_3D ( 'NONE', #31732, #21508, #23732 ) ;
#32801=CIRCLE ( 'NONE', #21403, 7.499999999999992895 ) ;
#32815=CIRCLE ( 'NONE', #23029, 2.500000000000000000 ) ;
#32840=DIRECTION ( 'NONE',  ( -1.000000000000000000, -0.000000000000000000, 0.000000000000000000 ) ) ;
#32869=VERTEX_POINT ( 'NONE', #5089 ) ;
#32923=ORIENTED_EDGE ( 'NONE', *, *, #13269, .T. ) ;
#32962=FACE_BOUND ( 'NONE', #26787, .T. ) ;
#32983=CARTESIAN_POINT ( 'NONE',  ( -65.20000000000000284, -0.9203920079924744480, -19.30000000000004690 ) ) ;
#32997=FACE_OUTER_BOUND ( 'NONE', #16864, .T. ) ;
#33023=VECTOR ( 'NONE', #18392, 1000.000000000000000 ) ;
#33029=EDGE_CURVE ( 'NONE', #33215, #2474, #32801, .T. ) ;
#33085=EDGE_CURVE ( 'NONE', #3502, #8327, #3996, .T. ) ;
#33215=VERTEX_POINT ( 'NONE', #20369 ) ;
#33217=CARTESIAN_POINT ( 'NONE',  ( -60.00000000000000000, -7.347880794884118356E-15, 20.00000000000001776 ) ) ;
#33259=DIRECTION ( 'NONE',  ( 0.000000000000000000, 0.000000000000000000, 1.000000000000000000 ) ) ;
#33269=DIRECTION ( 'NONE',  ( -1.000000000000000000, 0.000000000000000000, 0.000000000000000000 ) ) ;
#33287=VECTOR ( 'NONE', #5495, 1000.000000000000000 ) ;
#33293=ORIENTED_EDGE ( 'NONE', *, *, #26600, .F. ) ;
#33308=VERTEX_POINT ( 'NONE', #33311 ) ;
#33311=CARTESIAN_POINT ( 'NONE',  ( -52.50000000000002132, 155.0000000000000000, -16.99999999999999645 ) ) ;
#33358=SURFACE_SIDE_STYLE ('',( #7466 ) ) ;
#33359=CARTESIAN_POINT ( 'NONE',  ( -52.50000000000002132, 155.0000000000000000, 6.938893903907228378E-15 ) ) ;
#33391=CARTESIAN_POINT ( 'NONE',  ( -63.50000000000001421, 210.0000000000000000, -3.061616997868383141E-16 ) ) ;
#33400=ORIENTED_EDGE ( 'NONE', *, *, #26600, .T. ) ;
#33417=CARTESIAN_POINT ( 'NONE',  ( -62.70000000000000284, -88.00000000000000000, -20.00000000000000000 ) ) ;
#33441=AXIS2_PLACEMENT_3D ( 'NONE', #15635, #28260, #22970 ) ;
#33464=CARTESIAN_POINT ( 'NONE',  ( -65.20000000000000284, -0.9203920079924774456, 19.30000000000001847 ) ) ;
#33499=DIRECTION ( 'NONE',  ( -0.000000000000000000, 0.000000000000000000, -1.000000000000000000 ) ) ;
#33514=CARTESIAN_POINT ( 'NONE',  ( -56.01643337169826964, 194.9989636249862599, -0.3293050612182487069 ) ) ;
#33577=CARTESIAN_POINT ( 'NONE',  ( -66.50402289005056389, 121.5305141831588003, -17.99597710994943967 ) ) ;
#33590=CARTESIAN_POINT ( 'NONE',  ( -64.50000000000000000, 120.3589838486224437, 20.00000000000000000 ) ) ;
#33603=ORIENTED_EDGE ( 'NONE', *, *, #11020, .F. ) ;
#33639=DIRECTION ( 'NONE',  ( 1.000000000000000000, 0.000000000000000000, -0.000000000000000000 ) ) ;
#33646=LINE ( 'NONE', #12354, #10195 ) ;
#33666=CARTESIAN_POINT ( 'NONE',  ( -64.50000000000000000, 0.000000000000000000, -20.00000000000000000 ) ) ;
ENDSEC;
END-ISO-10303-21;
